ISO-10303-21;
HEADER;
FILE_DESCRIPTION (('STEP AP214'),
    '1' );
FILE_NAME ('Snap Open Cable Crossbars 3.step',
    '2026-10-08T22:59:04',
    ( '' ),
    ( '' ),
    'SwSTEP 2.0',
    'SolidWorks 2020',
    '' );
FILE_SCHEMA (( 'AUTOMOTIVE_DESIGN' ));
ENDSEC;

DATA;
#192=EDGE_CURVE ( 'NONE', #72719, #31733, #199411, .T. ) ;
#193=CARTESIAN_POINT ( 'NONE',  ( -18.40000000000000213, 11.47316190337364183, -91.25000000000005684 ) ) ;
#292=ORIENTED_EDGE ( 'NONE', *, *, #254482, .F. ) ;
#306=CARTESIAN_POINT ( 'NONE',  ( -16.81931177881022421, 9.936996059515065483, -87.77321787861730229 ) ) ;
#315=DIRECTION ( 'NONE',  ( -0.000000000000000000, 1.000000000000000000, -0.000000000000000000 ) ) ;
#362=CARTESIAN_POINT ( 'NONE',  ( -16.92570016628983609, 9.958788957751020021, -79.62065067003905483 ) ) ;
#434=CARTESIAN_POINT ( 'NONE',  ( -16.84421487269769102, 9.950000000011138823, -79.66950212244499596 ) ) ;
#1466=CARTESIAN_POINT ( 'NONE',  ( -16.98495255085919098, 10.00556436600592924, -79.63461720622055395 ) ) ;
#1483=DIRECTION ( 'NONE',  ( -0.000000000000000000, 1.000000000000000000, -0.000000000000000000 ) ) ;
#1646=DIRECTION ( 'NONE',  ( 0.000000000000000000, 1.000000000000000000, 0.000000000000000000 ) ) ;
#1805=VERTEX_POINT ( 'NONE', #42428 ) ;
#2425=AXIS2_PLACEMENT_3D ( 'NONE', #153513, #135160, #16531 ) ;
#2435=VECTOR ( 'NONE', #158170, 1000.000000000000000 ) ;
#2485=AXIS2_PLACEMENT_3D ( 'NONE', #224032, #44134, #123671 ) ;
#2519=DIRECTION ( 'NONE',  ( -0.7071067811865456854, 0.7071067811865493491, 0.000000000000000000 ) ) ;
#2598=VERTEX_POINT ( 'NONE', #11410 ) ;
#2616=AXIS2_PLACEMENT_3D ( 'NONE', #17562, #59224, #140067 ) ;
#2673=EDGE_CURVE ( 'NONE', #1805, #203569, #247284, .T. ) ;
#2787=CARTESIAN_POINT ( 'NONE',  ( -12.25000000000000178, 9.850000000011133849, -83.75000000000004263 ) ) ;
#2866=CARTESIAN_POINT ( 'NONE',  ( -16.87372397896795562, 9.880599536652887593, -87.35072451003577498 ) ) ;
#3112=EDGE_CURVE ( 'NONE', #172515, #48110, #11692, .T. ) ;
#3156=CARTESIAN_POINT ( 'NONE',  ( -16.87683809663752399, 9.950000000011137047, -87.09763598180374800 ) ) ;
#3167=VERTEX_POINT ( 'NONE', #31960 ) ;
#3743=EDGE_CURVE ( 'NONE', #108503, #194746, #27319, .T. ) ;
#3745=VERTEX_POINT ( 'NONE', #105366 ) ;
#3750=CARTESIAN_POINT ( 'NONE',  ( 13.22261339317536333, 9.436552840015579591, -82.17795547276035961 ) ) ;
#3886=EDGE_CURVE ( 'NONE', #23293, #73958, #175665, .T. ) ;
#3926=DIRECTION ( 'NONE',  ( 0.000000000000000000, 0.000000000000000000, -1.000000000000000000 ) ) ;
#3979=ADVANCED_FACE ( 'NONE', ( #36157 ), #255129, .F. ) ;
#4044=EDGE_CURVE ( 'NONE', #218042, #236168, #21721, .T. ) ;
#4365=CARTESIAN_POINT ( 'NONE',  ( -16.79363873026997922, 9.948850229429586634, -87.84615378144552267 ) ) ;
#4451=CARTESIAN_POINT ( 'NONE',  ( -16.79270642812319281, 9.946244216949068573, -87.83893327856206668 ) ) ;
#4730=CARTESIAN_POINT ( 'NONE',  ( -16.91256925476569606, 9.985731158139328656, -87.96764248900531413 ) ) ;
#4856=VECTOR ( 'NONE', #232844, 1000.000000000000000 ) ;
#4891=AXIS2_PLACEMENT_3D ( 'NONE', #94551, #97087, #98364 ) ;
#4907=CARTESIAN_POINT ( 'NONE',  ( -18.34374000495060386, 11.47316190337362585, -76.25000000000004263 ) ) ;
#5173=PLANE ( 'NONE',  #191830 ) ;
#5247=DIRECTION ( 'NONE',  ( -1.020425574104004196E-15, 0.000000000000000000, 1.000000000000000000 ) ) ;
#5295=DIRECTION ( 'NONE',  ( 0.5932847527679310229, -0.8049926720990042694, 0.000000000000000000 ) ) ;
#5314=CARTESIAN_POINT ( 'NONE',  ( 12.25000000000000000, 9.850000000011137402, -83.75000000000004263 ) ) ;
#5367=VERTEX_POINT ( 'NONE', #17576 ) ;
#5752=CARTESIAN_POINT ( 'NONE',  ( 20.73486653747088582, 7.250000000011182166, -79.65000000000004832 ) ) ;
#5995=DIRECTION ( 'NONE',  ( 0.7071067811865463515, -0.7071067811865487940, 0.000000000000000000 ) ) ;
#6195=LINE ( 'NONE', #66179, #251697 ) ;
#6380=FACE_OUTER_BOUND ( 'NONE', #50974, .T. ) ;
#6574=EDGE_CURVE ( 'NONE', #152148, #207925, #10893, .T. ) ;
#6685=ORIENTED_EDGE ( 'NONE', *, *, #206925, .T. ) ;
#6751=CARTESIAN_POINT ( 'NONE',  ( 18.54999999999999716, 8.750000000011182166, -87.85000000000003695 ) ) ;
#6793=ORIENTED_EDGE ( 'NONE', *, *, #91326, .F. ) ;
#7030=CARTESIAN_POINT ( 'NONE',  ( -16.93710578446422943, 9.950000000011137047, -87.58119601620070682 ) ) ;
#7090=( LENGTH_UNIT ( ) NAMED_UNIT ( * ) SI_UNIT ( .MILLI., .METRE. ) );
#7236=ORIENTED_EDGE ( 'NONE', *, *, #91337, .F. ) ;
#7244=ORIENTED_EDGE ( 'NONE', *, *, #66500, .T. ) ;
#7296=CARTESIAN_POINT ( 'NONE',  ( 23.24999999999999645, 8.822561741677553471, -79.65000000000004832 ) ) ;
#7399=CARTESIAN_POINT ( 'NONE',  ( -15.15564720441980739, 9.410708747058238899, -85.06920840584416510 ) ) ;
#7534=EDGE_LOOP ( 'NONE', ( #249804, #86820, #180964, #128455, #170519 ) ) ;
#7822=CARTESIAN_POINT ( 'NONE',  ( -21.64999999999999858, 9.350000000011133849, -79.65000000000004832 ) ) ;
#7925=EDGE_LOOP ( 'NONE', ( #42889, #247048, #205687, #26138 ) ) ;
#7983=CIRCLE ( 'NONE', #157858, 1.749999999999998002 ) ;
#8126=VERTEX_POINT ( 'NONE', #37459 ) ;
#8171=VECTOR ( 'NONE', #175043, 1000.000000000000000 ) ;
#8234=EDGE_LOOP ( 'NONE', ( #7236, #24725, #141993, #49067 ) ) ;
#8247=CARTESIAN_POINT ( 'NONE',  ( -16.78270389226384296, 9.947372616628161524, -87.84120703691151277 ) ) ;
#8410=EDGE_CURVE ( 'NONE', #78107, #56045, #231497, .T. ) ;
#8612=CARTESIAN_POINT ( 'NONE',  ( -16.94107738177414291, 10.01423928514777373, -87.95000000000004547 ) ) ;
#8685=UNCERTAINTY_MEASURE_WITH_UNIT (LENGTH_MEASURE( 1.000000000000000082E-05 ), #87038, 'distance_accuracy_value', 'NONE');
#8697=CARTESIAN_POINT ( 'NONE',  ( 23.04999999999999716, 8.822561741677553471, -91.25000000000005684 ) ) ;
#8698=CARTESIAN_POINT ( 'NONE',  ( -12.33960340485503338, 9.360749169926259938, -84.31457014060730160 ) ) ;
#8853=DIRECTION ( 'NONE',  ( 0.000000000000000000, -1.000000000000000000, 0.000000000000000000 ) ) ;
#8859=DIRECTION ( 'NONE',  ( -1.000000000000000000, 0.000000000000000000, -1.020425574104004196E-15 ) ) ;
#9001=AXIS2_PLACEMENT_3D ( 'NONE', #207166, #123773, #168075 ) ;
#9177=ORIENTED_EDGE ( 'NONE', *, *, #169214, .T. ) ;
#9542=ORIENTED_EDGE ( 'NONE', *, *, #257419, .T. ) ;
#9615=EDGE_LOOP ( 'NONE', ( #24514, #22576 ) ) ;
#9670=CARTESIAN_POINT ( 'NONE',  ( -16.93388492042258875, 9.988541822527059466, -79.59945487681387988 ) ) ;
#9980=CARTESIAN_POINT ( 'NONE',  ( -14.77538296656415007, 9.436662931810239741, -85.32303673229492347 ) ) ;
#10101=CARTESIAN_POINT ( 'NONE',  ( -14.00000000000000178, 9.850000000011133849, -83.75000000000004263 ) ) ;
#10307=DIRECTION ( 'NONE',  ( 1.000000000000000000, 0.000000000000000000, -0.000000000000000000 ) ) ;
#10382=EDGE_CURVE ( 'NONE', #248456, #219674, #191730, .T. ) ;
#10453=CARTESIAN_POINT ( 'NONE',  ( -16.97683809663752186, 9.950000000011138823, -87.09763598180373378 ) ) ;
#10526=ORIENTED_EDGE ( 'NONE', *, *, #29726, .F. ) ;
#10831=CARTESIAN_POINT ( 'NONE',  ( -23.25000000000000355, 5.650000000011139001, -87.85000000000003695 ) ) ;
#10893=CIRCLE ( 'NONE', #2485, 1.500000000000001332 ) ;
#10998=CIRCLE ( 'NONE', #2616, 1.500000000000001332 ) ;
#11065=EDGE_CURVE ( 'NONE', #39843, #242585, #226324, .T. ) ;
#11137=CARTESIAN_POINT ( 'NONE',  ( -15.15766958671844300, 9.410538608540024441, -82.43268799714094541 ) ) ;
#11270=CARTESIAN_POINT ( 'NONE',  ( -15.39126916658602973, 9.389571634557565716, -84.81764071236919733 ) ) ;
#11294=CARTESIAN_POINT ( 'NONE',  ( -16.92132318717937522, 9.966070024017081863, -79.62240663035211696 ) ) ;
#11321=LINE ( 'NONE', #171710, #147862 ) ;
#11332=EDGE_CURVE ( 'NONE', #41600, #206025, #125346, .T. ) ;
#11410=CARTESIAN_POINT ( 'NONE',  ( 18.39999999999999503, 11.75000000001113953, -91.25000000000005684 ) ) ;
#11580=EDGE_LOOP ( 'NONE', ( #63865, #9542, #128841, #112694, #46605, #161713, #246046, #167279, #50674 ) ) ;
#11692=( BOUNDED_CURVE ( )  B_SPLINE_CURVE ( 3, ( #76179, #172774, #33254, #155764 ),
 .UNSPECIFIED., .F., .T. ) 
 B_SPLINE_CURVE_WITH_KNOTS ( ( 4, 4 ),
 ( 3.432212674861197410, 3.693332928900581624 ),
 .UNSPECIFIED. ) 
 CURVE ( )  GEOMETRIC_REPRESENTATION_ITEM ( )  RATIONAL_B_SPLINE_CURVE ( ( 1.000000000000000000, 0.9943260843901261525, 0.9943260843901261525, 1.000000000000000000 ) ) 
 REPRESENTATION_ITEM ( '' )  );
#11713=VECTOR ( 'NONE', #29030, 1000.000000000000000 ) ;
#12288=CARTESIAN_POINT ( 'NONE',  ( -16.93583594267724024, 10.00862343506335783, -79.55939083932079825 ) ) ;
#12296=ORIENTED_EDGE ( 'NONE', *, *, #238093, .F. ) ;
#12439=CARTESIAN_POINT ( 'NONE',  ( -14.11697426661281440, 9.457410944778569473, -82.00008397379009750 ) ) ;
#12668=DIRECTION ( 'NONE',  ( -0.7071067811865487940, 0.7071067811865463515, -7.215498431451184074E-16 ) ) ;
#12812=( BOUNDED_SURFACE ( )  B_SPLINE_SURFACE ( 3, 2, ( 
 ( #85535, #4730, #8612 ),
 ( #145537, #47716, #225061 ),
 ( #64725, #46436, #88108 ),
 ( #162567, #122143, #141687 ) ),
 .UNSPECIFIED., .F., .F., .F. ) 
 B_SPLINE_SURFACE_WITH_KNOTS ( ( 4, 4 ),
 ( 3, 3 ),
 ( 0.0008258556059633754111, 0.0009616864997632845833 ),
 ( 0.000000000000000000, 1.000000000000000000 ),
 .UNSPECIFIED. ) 
 GEOMETRIC_REPRESENTATION_ITEM ( )  RATIONAL_B_SPLINE_SURFACE ( (
 ( 1.000000000000000000, 0.9152888060719349683, 1.000000000000000000),
 ( 1.000000000000000000, 0.9327727094138200670, 1.000000000000000000),
 ( 1.000000000000000000, 0.9369023509258446181, 1.000000000000000000),
 ( 1.000000000000000000, 0.9246339933864486937, 1.000000000000000000) ) ) 
 REPRESENTATION_ITEM ( '' )  SURFACE ( )  );
#13098=CARTESIAN_POINT ( 'NONE',  ( 15.66039659514495774, 9.360749169926259938, -84.31457014060728739 ) ) ;
#13383=ADVANCED_FACE ( 'NONE', ( #249847 ), #112905, .F. ) ;
#13389=ORIENTED_EDGE ( 'NONE', *, *, #202066, .T. ) ;
#13562=CARTESIAN_POINT ( 'NONE',  ( -16.93772744219066340, 9.993541108763510650, -79.59806197196974153 ) ) ;
#13912=VERTEX_POINT ( 'NONE', #194396 ) ;
#14073=EDGE_LOOP ( 'NONE', ( #160139, #57208, #110758, #102427, #124497 ) ) ;
#14174=CARTESIAN_POINT ( 'NONE',  ( -16.87036670365549895, 9.989418819312803066, -79.52043988269799968 ) ) ;
#14274=DIRECTION ( 'NONE',  ( 1.000000000000000000, 0.000000000000000000, 0.000000000000000000 ) ) ;
#14484=CARTESIAN_POINT ( 'NONE',  ( -18.34374000495059676, 11.47316190337362940, -91.25000000000005684 ) ) ;
#14549=EDGE_CURVE ( 'NONE', #102764, #67043, #71255, .T. ) ;
#14621=VERTEX_POINT ( 'NONE', #38535 ) ;
#14645=DIRECTION ( 'NONE',  ( -0.000000000000000000, -0.000000000000000000, -1.000000000000000000 ) ) ;
#14766=ORIENTED_EDGE ( 'NONE', *, *, #26669, .T. ) ;
#14921=CARTESIAN_POINT ( 'NONE',  ( -18.39999999999999858, 11.47316190337362762, -76.32594606680801519 ) ) ;
#15045=CYLINDRICAL_SURFACE ( 'NONE', #4891, 0.1000000000000013656 ) ;
#15128=CARTESIAN_POINT ( 'NONE',  ( -16.97683809663752186, 9.950000000011138823, -76.25000000000004263 ) ) ;
#15340=DIRECTION ( 'NONE',  ( -1.000000000000000000, 3.854941057726231589E-15, 0.000000000000000000 ) ) ;
#15433=PLANE ( 'NONE',  #75039 ) ;
#15681=CARTESIAN_POINT ( 'NONE',  ( 13.12229106158773284, 9.430637101707896264, -85.26826061806100654 ) ) ;
#15735=ADVANCED_FACE ( 'NONE', ( #174277 ), #197629, .F. ) ;
#15882=ORIENTED_EDGE ( 'NONE', *, *, #69037, .T. ) ;
#15978=PLANE ( 'NONE',  #111246 ) ;
#15988=CIRCLE ( 'NONE', #20244, 0.9000000000000014655 ) ;
#16094=CARTESIAN_POINT ( 'NONE',  ( -16.89935556175729303, 9.950000000011135270, -80.13967636288485608 ) ) ;
#16402=CARTESIAN_POINT ( 'NONE',  ( -16.86420534634261514, 9.970615445602874161, -87.91833654923743779 ) ) ;
#16531=DIRECTION ( 'NONE',  ( 1.000000000000000000, 0.000000000000000000, 0.000000000000000000 ) ) ;
#16603=CARTESIAN_POINT ( 'NONE',  ( -16.86337532320262156, 9.979967204235514089, -79.55107553101724704 ) ) ;
#16828=VECTOR ( 'NONE', #220213, 1000.000000000000000 ) ;
#17043=CARTESIAN_POINT ( 'NONE',  ( -23.25000000000000355, 5.650000000011139001, -79.65000000000004832 ) ) ;
#17178=DIRECTION ( 'NONE',  ( -0.000000000000000000, -0.000000000000000000, -1.000000000000000000 ) ) ;
#17186=FACE_OUTER_BOUND ( 'NONE', #80253, .T. ) ;
#17244=DIRECTION ( 'NONE',  ( 0.7071067811865463515, 0.7071067811865487940, 7.587431340288849180E-16 ) ) ;
#17300=EDGE_LOOP ( 'NONE', ( #59593, #211163, #127519, #111959 ) ) ;
#17316=VERTEX_POINT ( 'NONE', #210266 ) ;
#17365=CARTESIAN_POINT ( 'NONE',  ( -21.65000000000000213, 9.950000000011140600, -87.75000000000005684 ) ) ;
#17484=EDGE_CURVE ( 'NONE', #77128, #125903, #119851, .T. ) ;
#17562=CARTESIAN_POINT ( 'NONE',  ( 20.04999999999999716, 8.750000000011173285, -79.65000000000004832 ) ) ;
#17576=CARTESIAN_POINT ( 'NONE',  ( -18.40000000000000213, 11.47316190337364183, -91.17405393319209850 ) ) ;
#17657=DIRECTION ( 'NONE',  ( -1.646408749285562691E-14, 1.000000000000000000, 0.000000000000000000 ) ) ;
#17776=SURFACE_STYLE_USAGE ( .BOTH. , #136431 ) ;
#17790=EDGE_LOOP ( 'NONE', ( #165832, #248407, #230577, #193376 ) ) ;
#17805=CARTESIAN_POINT ( 'NONE',  ( -17.05016517656156694, 9.950000000013657697, -87.82730200399912235 ) ) ;
#18040=B_SPLINE_CURVE_WITH_KNOTS ( 'NONE', 3,
 ( #123895, #67759, #26079, #105565, #127745, #63911, #187730, #27392, #147294, #143441 ),
 .UNSPECIFIED., .F., .F.,
 ( 4, 3, 3, 4 ),
 ( 1.957469226477651626E-15, 8.145022132839031210E-06, 1.905645951092787237E-05, 2.061107371226127689E-05 ),
 .UNSPECIFIED. ) ;
#18290=DIRECTION ( 'NONE',  ( -1.073024830501117725E-15, -0.000000000000000000, -1.000000000000000000 ) ) ;
#18588=SHAPE_REPRESENTATION ( 'Snap Open Cable Crossbars 3', ( #2425 ), #27429 ) ;
#18628=CARTESIAN_POINT ( 'NONE',  ( -16.92280123533722858, 9.950000000011137047, -79.85063231408514639 ) ) ;
#18895=AXIS2_PLACEMENT_3D ( 'NONE', #90973, #110535, #47992 ) ;
#18986=CARTESIAN_POINT ( 'NONE',  ( -16.89081410710458542, 9.951318529858268036, -87.85440591983640957 ) ) ;
#19080=ORIENTED_EDGE ( 'NONE', *, *, #80881, .F. ) ;
#19248=ORIENTED_EDGE ( 'NONE', *, *, #3112, .F. ) ;
#19327=DIRECTION ( 'NONE',  ( -1.000000000000000000, 0.000000000000000000, 0.000000000000000000 ) ) ;
#19469=ORIENTED_EDGE ( 'NONE', *, *, #157483, .F. ) ;
#19954=CARTESIAN_POINT ( 'NONE',  ( -16.92973740335372668, 9.992503814478325808, -79.59394096479805114 ) ) ;
#19962=CARTESIAN_POINT ( 'NONE',  ( -16.80468759584937999, 9.942153675145297242, -79.69001886620168307 ) ) ;
#20099=DIRECTION ( 'NONE',  ( -0.000000000000000000, -0.000000000000000000, -1.000000000000000000 ) ) ;
#20244=AXIS2_PLACEMENT_3D ( 'NONE', #182348, #186190, #241036 ) ;
#20247=CARTESIAN_POINT ( 'NONE',  ( -16.89268316805465986, 9.951721813253337601, -87.85575247854558256 ) ) ;
#20252=CARTESIAN_POINT ( 'NONE',  ( -16.89268316805466341, 9.951721813253341153, -79.64424752145448849 ) ) ;
#20254=CARTESIAN_POINT ( 'NONE',  ( -16.87036670365549895, 10.08494996326643189, -79.55000000000005400 ) ) ;
#20350=ORIENTED_EDGE ( 'NONE', *, *, #170187, .T. ) ;
#20502=VECTOR ( 'NONE', #20099, 1000.000000000000000 ) ;
#20682=CARTESIAN_POINT ( 'NONE',  ( 20.73486653747088582, 7.250000000011182166, -76.25000000000004263 ) ) ;
#20728=EDGE_LOOP ( 'NONE', ( #146061, #119987, #108509, #216571 ) ) ;
#20769=CARTESIAN_POINT ( 'NONE',  ( 14.77516762759922031, 9.436674251854004325, -82.17686193099926584 ) ) ;
#21073=CARTESIAN_POINT ( 'NONE',  ( -16.94445028196808778, 9.992063609708889516, -79.60733017841850767 ) ) ;
#21174=DIRECTION ( 'NONE',  ( 1.000000000000000000, 0.000000000000000000, -0.000000000000000000 ) ) ;
#21210=ORIENTED_EDGE ( 'NONE', *, *, #23504, .F. ) ;
#21239=DIRECTION ( 'NONE',  ( 1.186688945009010077E-16, -1.000000000000000000, -0.000000000000000000 ) ) ;
#21250=CARTESIAN_POINT ( 'NONE',  ( 20.73486653747088937, 7.750000000011182166, -76.25000000000004263 ) ) ;
#21254=CARTESIAN_POINT ( 'NONE',  ( -16.86445178670638967, 9.962211629127175172, -79.60922256188266033 ) ) ;
#21261=LINE ( 'NONE', #98156, #255974 ) ;
#21321=LINE ( 'NONE', #47250, #115600 ) ;
#21480=FACE_OUTER_BOUND ( 'NONE', #214458, .T. ) ;
#21518=EDGE_CURVE ( 'NONE', #194746, #72719, #159532, .T. ) ;
#21577=CARTESIAN_POINT ( 'NONE',  ( -17.22767730082871296, 10.34924421247856863, -89.14242869057068219 ) ) ;
#21597=EDGE_CURVE ( 'NONE', #207925, #175274, #21321, .T. ) ;
#21721=LINE ( 'NONE', #159963, #198150 ) ;
#21829=VECTOR ( 'NONE', #162973, 1000.000000000000000 ) ;
#22148=ORIENTED_EDGE ( 'NONE', *, *, #205331, .F. ) ;
#22260=ORIENTED_EDGE ( 'NONE', *, *, #2673, .T. ) ;
#22395=CIRCLE ( 'NONE', #168170, 0.1000000000000028644 ) ;
#22576=ORIENTED_EDGE ( 'NONE', *, *, #215047, .T. ) ;
#22804=AXIS2_PLACEMENT_3D ( 'NONE', #235757, #254035, #196632 ) ;
#22998=ORIENTED_EDGE ( 'NONE', *, *, #183258, .T. ) ;
#23008=ORIENTED_EDGE ( 'NONE', *, *, #138298, .T. ) ;
#23139=VECTOR ( 'NONE', #63876, 1000.000000000000000 ) ;
#23293=VERTEX_POINT ( 'NONE', #192428 ) ;
#23349=CARTESIAN_POINT ( 'NONE',  ( 15.70340296795548518, 9.355888454513701546, -83.28864289677805743 ) ) ;
#23504=EDGE_CURVE ( 'NONE', #185121, #1805, #91583, .T. ) ;
#23508=CARTESIAN_POINT ( 'NONE',  ( -16.87036670365548474, 9.989418819312801290, -87.97956011730209980 ) ) ;
#23598=DIRECTION ( 'NONE',  ( -1.000000000000000000, 0.000000000000000000, 0.000000000000000000 ) ) ;
#23900=CARTESIAN_POINT ( 'NONE',  ( -16.81744102076749314, 9.950000000011142376, -79.65000000000004832 ) ) ;
#23934=ORIENTED_EDGE ( 'NONE', *, *, #10382, .F. ) ;
#24025=CARTESIAN_POINT ( 'NONE',  ( 15.74999999999999645, 9.350000000011139178, -83.75000000000004263 ) ) ;
#24427=LINE ( 'NONE', #205584, #129347 ) ;
#24514=ORIENTED_EDGE ( 'NONE', *, *, #215165, .T. ) ;
#24725=ORIENTED_EDGE ( 'NONE', *, *, #126357, .F. ) ;
#24916=CARTESIAN_POINT ( 'NONE',  ( -17.11825945287482753, 10.05000000001113847, -79.65000000000004832 ) ) ;
#24918=PLANE ( 'NONE',  #95315 ) ;
#25003=CARTESIAN_POINT ( 'NONE',  ( -18.40000000000000213, 11.41458325961093756, -79.65000000000004832 ) ) ;
#25237=DIRECTION ( 'NONE',  ( -1.652117596168391700E-15, -1.000000000000000000, 0.000000000000000000 ) ) ;
#25396=ORIENTED_EDGE ( 'NONE', *, *, #25746, .T. ) ;
#25746=EDGE_CURVE ( 'NONE', #170888, #152148, #27875, .T. ) ;
#25786=CARTESIAN_POINT ( 'NONE',  ( -18.40000000000000213, 11.33174054713631662, -79.65000000000004832 ) ) ;
#25898=CARTESIAN_POINT ( 'NONE',  ( 15.06592377766031809, 9.417789466963361278, -82.35738454397692010 ) ) ;
#26039=EDGE_LOOP ( 'NONE', ( #178469, #59495 ) ) ;
#26079=CARTESIAN_POINT ( 'NONE',  ( -16.88815647973234135, 9.950832619326893891, -79.64721706332603901 ) ) ;
#26138=ORIENTED_EDGE ( 'NONE', *, *, #8410, .F. ) ;
#26203=CARTESIAN_POINT ( 'NONE',  ( -16.94275863006528482, 9.989496048678669027, -87.89169738207662874 ) ) ;
#26332=ORIENTED_EDGE ( 'NONE', *, *, #3743, .T. ) ;
#26592=CARTESIAN_POINT ( 'NONE',  ( -18.40000000000000213, 5.650000000011139001, -79.65000000000004832 ) ) ;
#26605=ORIENTED_EDGE ( 'NONE', *, *, #257419, .F. ) ;
#26620=CARTESIAN_POINT ( 'NONE',  ( -16.77180007708460963, 9.950000000011137047, -87.86438588104522296 ) ) ;
#26669=EDGE_CURVE ( 'NONE', #146715, #39843, #120586, .T. ) ;
#26686=SURFACE_STYLE_USAGE ( .BOTH. , #238322 ) ;
#26768=ADVANCED_FACE ( 'NONE', ( #183120 ), #47429, .F. ) ;
#26913=ORIENTED_EDGE ( 'NONE', *, *, #184992, .T. ) ;
#26942=CYLINDRICAL_SURFACE ( 'NONE', #54985, 14.30833333333333890 ) ;
#26994=DIRECTION ( 'NONE',  ( -0.000000000000000000, -0.000000000000000000, -1.000000000000000000 ) ) ;
#27005=CARTESIAN_POINT ( 'NONE',  ( -14.11361717019515893, 9.457426452500060421, -85.50004186840004650 ) ) ;
#27166=FACE_OUTER_BOUND ( 'NONE', #87862, .T. ) ;
#27285=DIRECTION ( 'NONE',  ( -1.186688945009010077E-16, 1.000000000000000000, 0.000000000000000000 ) ) ;
#27319=CIRCLE ( 'NONE', #18895, 0.9000000000000014655 ) ;
#27365=ORIENTED_EDGE ( 'NONE', *, *, #69037, .F. ) ;
#27392=CARTESIAN_POINT ( 'NONE',  ( -16.87435696428308063, 9.950002462943377424, -79.64999176516661805 ) ) ;
#27429=( GEOMETRIC_REPRESENTATION_CONTEXT ( 3 ) GLOBAL_UNCERTAINTY_ASSIGNED_CONTEXT ( ( #8685 ) ) GLOBAL_UNIT_ASSIGNED_CONTEXT ( ( #87038, #169206, #213418 ) ) REPRESENTATION_CONTEXT ( 'NONE', 'WORKASPACE' ) );
#27832=CARTESIAN_POINT ( 'NONE',  ( -16.80939487329394666, 9.950000000011138823, -87.85000000000093223 ) ) ;
#27875=LINE ( 'NONE', #31728, #117785 ) ;
#27989=FACE_OUTER_BOUND ( 'NONE', #217340, .T. ) ;
#28002=LINE ( 'NONE', #107497, #206484 ) ;
#28285=DIRECTION ( 'NONE',  ( 1.000000000000000000, 0.000000000000000000, -0.000000000000000000 ) ) ;
#28293=ORIENTED_EDGE ( 'NONE', *, *, #142597, .T. ) ;
#28622=CARTESIAN_POINT ( 'NONE',  ( -17.01473183483382101, 9.950000000011138823, -79.75000000000005684 ) ) ;
#28743=AXIS2_PLACEMENT_3D ( 'NONE', #102887, #119947, #125057 ) ;
#28748=LINE ( 'NONE', #228190, #220018 ) ;
#28760=VERTEX_POINT ( 'NONE', #138868 ) ;
#28770=ORIENTED_EDGE ( 'NONE', *, *, #180393, .T. ) ;
#29030=DIRECTION ( 'NONE',  ( 0.000000000000000000, -1.000000000000000000, 0.000000000000000000 ) ) ;
#29031=ORIENTED_EDGE ( 'NONE', *, *, #202066, .F. ) ;
#29077=CARTESIAN_POINT ( 'NONE',  ( 23.24999999999999645, 8.822561741677553471, -87.85000000000003695 ) ) ;
#29285=CARTESIAN_POINT ( 'NONE',  ( -16.95709691156492127, 9.950000000011140600, -79.66005756250774539 ) ) ;
#29302=CARTESIAN_POINT ( 'NONE',  ( -16.93255653858138388, 9.998451453988312920, -79.58164336798972727 ) ) ;
#29363=EDGE_CURVE ( 'NONE', #2598, #187000, #225818, .T. ) ;
#29726=EDGE_CURVE ( 'NONE', #52869, #241355, #109871, .T. ) ;
#29806=CARTESIAN_POINT ( 'NONE',  ( 22.88900146558018989, 8.703904791123973084, -87.85000000000003695 ) ) ;
#29816=FACE_OUTER_BOUND ( 'NONE', #154389, .T. ) ;
#30044=CARTESIAN_POINT ( 'NONE',  ( -16.87242674293849021, 9.950000000011138823, -87.85109024637240793 ) ) ;
#30086=CARTESIAN_POINT ( 'NONE',  ( -16.93415306273742260, 9.995622260023671046, -87.91005694236046963 ) ) ;
#30515=CARTESIAN_POINT ( 'NONE',  ( -17.01473183483379970, 9.950000000011140600, -87.75000000000005684 ) ) ;
#30682=EDGE_CURVE ( 'NONE', #108130, #146336, #137058, .T. ) ;
#30700=FACE_OUTER_BOUND ( 'NONE', #232365, .T. ) ;
#30762=CARTESIAN_POINT ( 'NONE',  ( -18.40000000000000213, 11.48667500176882328, -76.25000000000004263 ) ) ;
#30789=VECTOR ( 'NONE', #32892, 1000.000000000000000 ) ;
#30818=CARTESIAN_POINT ( 'NONE',  ( -16.81095280782811230, 9.950000000011138823, -79.64999999999918145 ) ) ;
#31425=EDGE_CURVE ( 'NONE', #5367, #52869, #137050, .T. ) ;
#31728=CARTESIAN_POINT ( 'NONE',  ( 18.54999999999999716, 8.750000000011182166, -76.25000000000004263 ) ) ;
#31733=VERTEX_POINT ( 'NONE', #5752 ) ;
#31817=CARTESIAN_POINT ( 'NONE',  ( -12.25000000000000178, 9.850000000011133849, -83.75000000000004263 ) ) ;
#31960=CARTESIAN_POINT ( 'NONE',  ( 18.54999999999999716, 9.950000000011153034, -79.64999999999999147 ) ) ;
#31980=CARTESIAN_POINT ( 'NONE',  ( -17.80356949363855179, 10.87673139701218616, -77.28692697577338322 ) ) ;
#31996=AXIS2_PLACEMENT_3D ( 'NONE', #248910, #149819, #10307 ) ;
#31997=CARTESIAN_POINT ( 'NONE',  ( 21.13736287352038445, 8.046642376395153562, -87.85000000000003695 ) ) ;
#32320=DIRECTION ( 'NONE',  ( 1.000000000000000000, -0.000000000000000000, -0.000000000000000000 ) ) ;
#32384=DIRECTION ( 'NONE',  ( 1.000000000000000000, 1.186688945009010077E-16, 0.000000000000000000 ) ) ;
#32892=DIRECTION ( 'NONE',  ( -0.000000000000000000, -0.000000000000000000, -1.000000000000000000 ) ) ;
#32916=CARTESIAN_POINT ( 'NONE',  ( 23.04999999999999716, 8.822561741677553471, -76.25000000000004263 ) ) ;
#32954=VERTEX_POINT ( 'NONE', #102638 ) ;
#32989=ORIENTED_EDGE ( 'NONE', *, *, #68262, .T. ) ;
#33254=CARTESIAN_POINT ( 'NONE',  ( 17.74533788810829904, 10.81849979148195118, -90.18637732505249005 ) ) ;
#33304=CARTESIAN_POINT ( 'NONE',  ( -15.06774609480955895, 9.417651958852161442, -82.35878739244051872 ) ) ;
#33855=CARTESIAN_POINT ( 'NONE',  ( 18.39999999999999503, 5.650000000011139001, -87.85000000000003695 ) ) ;
#33929=ADVANCED_FACE ( 'NONE', ( #72920 ), #114583, .T. ) ;
#34432=CARTESIAN_POINT ( 'NONE',  ( -16.93970660449832621, 10.01284139164672915, -79.55228173579450868 ) ) ;
#34566=CARTESIAN_POINT ( 'NONE',  ( -12.29659703204451660, 9.355888454513703323, -83.28864289677802901 ) ) ;
#34731=CARTESIAN_POINT ( 'NONE',  ( -16.94275863009466576, 9.989496048673542461, -79.60830261795892682 ) ) ;
#35247=CARTESIAN_POINT ( 'NONE',  ( 14.22916352759893321, 9.457410930301314522, -85.49991590874631697 ) ) ;
#35734=B_SPLINE_CURVE_WITH_KNOTS ( 'NONE', 3,
 ( #213027, #111367, #150502, #173961, #69691, #13562, #190931, #113927, #230028, #29302, #130928, #53952, #133495, #108789, #12288, #231333, #34432, #52660, #89224 ),
 .UNSPECIFIED., .F., .F.,
 ( 4, 3, 3, 3, 3, 3, 4 ),
 ( 0.0001624081864585800018, 0.0001685232196531700956, 0.0001764526673566917288, 0.0001916878551483148813, 0.0002009890782182524550, 0.0002238845907555116882, 0.0002283406619926272728 ),
 .UNSPECIFIED. ) ;
#35939=LINE ( 'NONE', #175457, #206576 ) ;
#36002=CARTESIAN_POINT ( 'NONE',  ( -16.92925196614875816, 9.972331796421277872, -79.61674484771684490 ) ) ;
#36094=( NAMED_UNIT ( * ) PLANE_ANGLE_UNIT ( ) SI_UNIT ( $, .RADIAN. ) );
#36157=FACE_OUTER_BOUND ( 'NONE', #50649, .T. ) ;
#36949=CARTESIAN_POINT ( 'NONE',  ( -16.82055514392378726, 9.950000000011137047, -79.67679807454184981 ) ) ;
#37295=CARTESIAN_POINT ( 'NONE',  ( -18.41431012584569160, 11.48747202921933130, -91.27323601310172307 ) ) ;
#37405=CARTESIAN_POINT ( 'NONE',  ( -16.97092634996655747, 10.00088896635952196, -87.86985723370234780 ) ) ;
#37459=CARTESIAN_POINT ( 'NONE',  ( -16.81744102076748959, 9.950000000011138823, -87.85000000000005116 ) ) ;
#37915=ORIENTED_EDGE ( 'NONE', *, *, #157840, .T. ) ;
#38024=CARTESIAN_POINT ( 'NONE',  ( -23.25000000000000355, 10.05000000001113847, -79.75000000000004263 ) ) ;
#38097=CARTESIAN_POINT ( 'NONE',  ( 22.88900146558018989, 8.703904791123973084, -76.25000000000004263 ) ) ;
#38181=CARTESIAN_POINT ( 'NONE',  ( 21.72449340488909897, 10.28395627750227703, -87.85000000000003695 ) ) ;
#38535=CARTESIAN_POINT ( 'NONE',  ( -18.40000000000000213, 11.47316190337364183, -87.95000000000004547 ) ) ;
#38688=VERTEX_POINT ( 'NONE', #24025 ) ;
#38826=DIRECTION ( 'NONE',  ( 0.000000000000000000, -0.000000000000000000, -1.000000000000000000 ) ) ;
#39296=VERTEX_POINT ( 'NONE', #215174 ) ;
#39513=CARTESIAN_POINT ( 'NONE',  ( -16.84793658983432607, 9.950000000011140600, -79.73364667781054038 ) ) ;
#39564=ADVANCED_FACE ( 'NONE', ( #67653 ), #223850, .T. ) ;
#39843=VERTEX_POINT ( 'NONE', #235704 ) ;
#39870=CARTESIAN_POINT ( 'NONE',  ( -16.87036670365548474, 9.989418819312799513, -87.97956011730209980 ) ) ;
#40202=ORIENTED_EDGE ( 'NONE', *, *, #50756, .F. ) ;
#40269=EDGE_LOOP ( 'NONE', ( #229709, #183898, #19469, #255139 ) ) ;
#40320=LINE ( 'NONE', #175970, #16828 ) ;
#40791=CARTESIAN_POINT ( 'NONE',  ( -16.97683810757273193, 9.950000000011137047, -80.26357671246051950 ) ) ;
#40924=CARTESIAN_POINT ( 'NONE',  ( -20.65000000000000568, 7.250000000011138646, -76.25000000000004263 ) ) ;
#41063=ADVANCED_FACE ( 'NONE', ( #165202 ), #187349, .F. ) ;
#41600=VERTEX_POINT ( 'NONE', #94009 ) ;
#41621=CARTESIAN_POINT ( 'NONE',  ( 14.56326696814971022, 9.446648990640017729, -82.08916329592322825 ) ) ;
#42100=CARTESIAN_POINT ( 'NONE',  ( -16.81930730667006557, 9.936998068885204205, -79.72676773053824206 ) ) ;
#42149=ORIENTED_EDGE ( 'NONE', *, *, #127354, .F. ) ;
#42308=CARTESIAN_POINT ( 'NONE',  ( -16.84793658983420173, 9.950000000011138823, -87.76635332218982910 ) ) ;
#42422=VERTEX_POINT ( 'NONE', #185256 ) ;
#42428=CARTESIAN_POINT ( 'NONE',  ( -16.87683809663752399, 9.850000000011144508, -87.09763598180374800 ) ) ;
#42495=CARTESIAN_POINT ( 'NONE',  ( 20.27550659511089037, 9.216043722519994930, -87.85000000000003695 ) ) ;
#42779=ADVANCED_FACE ( 'NONE', ( #233395 ), #54726, .F. ) ;
#42889=ORIENTED_EDGE ( 'NONE', *, *, #245805, .F. ) ;
#43022=EDGE_CURVE ( 'NONE', #68524, #222707, #226710, .T. ) ;
#43323=LINE ( 'NONE', #122865, #242571 ) ;
#43358=FACE_OUTER_BOUND ( 'NONE', #149158, .T. ) ;
#43597=CARTESIAN_POINT ( 'NONE',  ( -16.88705144915409306, 9.950000000011138823, -87.56902140528751488 ) ) ;
#43599=VECTOR ( 'NONE', #47577, 1000.000000000000000 ) ;
#44134=DIRECTION ( 'NONE',  ( -1.073024830501117725E-15, 0.000000000000000000, 1.000000000000000000 ) ) ;
#44177=CARTESIAN_POINT ( 'NONE',  ( 15.15590539855246277, 9.410682294279109072, -82.43114344194833620 ) ) ;
#44342=ORIENTED_EDGE ( 'NONE', *, *, #141917, .F. ) ;
#44450=DIRECTION ( 'NONE',  ( -0.5932847527679299127, 0.8049926720990051576, 6.366092712777055223E-16 ) ) ;
#44585=ADVANCED_FACE ( 'NONE', ( #194970 ), #15045, .F. ) ;
#44607=DIRECTION ( 'NONE',  ( 0.000000000000000000, -1.000000000000000000, 0.000000000000000000 ) ) ;
#44808=AXIS2_PLACEMENT_3D ( 'NONE', #203322, #125073, #27285 ) ;
#44879=CARTESIAN_POINT ( 'NONE',  ( -16.89155683852633416, 9.950000000011138823, -87.22262815045961304 ) ) ;
#45279=CARTESIAN_POINT ( 'NONE',  ( 23.24999999999999645, 11.75000000001113953, -87.85000000000003695 ) ) ;
#45686=VERTEX_POINT ( 'NONE', #251051 ) ;
#45692=ORIENTED_EDGE ( 'NONE', *, *, #113535, .T. ) ;
#46153=CARTESIAN_POINT ( 'NONE',  ( -16.85697194749126027, 9.908543714134777858, -87.56499573238625089 ) ) ;
#46436=CARTESIAN_POINT ( 'NONE',  ( -16.90202395485779974, 9.965944544561983420, -87.90301372126040746 ) ) ;
#46605=ORIENTED_EDGE ( 'NONE', *, *, #242328, .T. ) ;
#46902=ORIENTED_EDGE ( 'NONE', *, *, #207289, .T. ) ;
#46940=CARTESIAN_POINT ( 'NONE',  ( -17.11825945287482753, 10.05000000001113847, -79.65000000000004832 ) ) ;
#46978=CARTESIAN_POINT ( 'NONE',  ( 21.72449340488910252, 10.28395627750227703, -79.65000000000004832 ) ) ;
#47030=CARTESIAN_POINT ( 'NONE',  ( -16.93234230245721861, 9.998107370558241058, -87.91769028166629596 ) ) ;
#47187=CARTESIAN_POINT ( 'NONE',  ( 18.39999999999999503, 11.75000000001113953, -91.25000000000005684 ) ) ;
#47241=CARTESIAN_POINT ( 'NONE',  ( 18.39999999999999147, 8.822561741677553471, -76.25000000000004263 ) ) ;
#47250=CARTESIAN_POINT ( 'NONE',  ( 20.73486653747090003, 7.250000000011182166, -87.85000000000003695 ) ) ;
#47337=CARTESIAN_POINT ( 'NONE',  ( -16.77683809663752257, 9.945835743215303282, -87.83605098089584828 ) ) ;
#47425=CARTESIAN_POINT ( 'NONE',  ( -16.77308656112214535, 9.950000000011135270, -87.84980680829774258 ) ) ;
#47429=PLANE ( 'NONE',  #55760 ) ;
#47577=DIRECTION ( 'NONE',  ( 1.000000000000000000, -0.000000000000000000, -0.000000000000000000 ) ) ;
#47667=CARTESIAN_POINT ( 'NONE',  ( -16.94445028196807002, 9.992063609708893068, -87.89266982158160602 ) ) ;
#47716=CARTESIAN_POINT ( 'NONE',  ( -16.89797118371612683, 9.976380722655340705, -87.93729336755826864 ) ) ;
#47725=VECTOR ( 'NONE', #100722, 1000.000000000000000 ) ;
#47898=LINE ( 'NONE', #83145, #180355 ) ;
#47963=EDGE_CURVE ( 'NONE', #17316, #241355, #72172, .T. ) ;
#47992=DIRECTION ( 'NONE',  ( -1.000000000000000000, 0.000000000000000000, 0.000000000000000000 ) ) ;
#48010=ORIENTED_EDGE ( 'NONE', *, *, #203075, .F. ) ;
#48053=ORIENTED_EDGE ( 'NONE', *, *, #111805, .T. ) ;
#48110=VERTEX_POINT ( 'NONE', #85315 ) ;
#48230=( GEOMETRIC_REPRESENTATION_CONTEXT ( 3 ) GLOBAL_UNCERTAINTY_ASSIGNED_CONTEXT ( ( #246015 ) ) GLOBAL_UNIT_ASSIGNED_CONTEXT ( ( #197710, #36094, #173072 ) ) REPRESENTATION_CONTEXT ( 'NONE', 'WORKASPACE' ) );
#48463=LINE ( 'NONE', #128019, #149529 ) ;
#48557=EDGE_LOOP ( 'NONE', ( #256331, #156146 ) ) ;
#48658=FACE_OUTER_BOUND ( 'NONE', #74185, .T. ) ;
#48787=DIRECTION ( 'NONE',  ( 0.000000000000000000, 0.000000000000000000, -1.000000000000000000 ) ) ;
#48876=AXIS2_PLACEMENT_3D ( 'NONE', #242394, #63761, #143299 ) ;
#48911=EDGE_LOOP ( 'NONE', ( #181641, #32989, #130963, #151672, #159964 ) ) ;
#48963=EDGE_CURVE ( 'NONE', #201212, #42422, #91158, .T. ) ;
#49067=ORIENTED_EDGE ( 'NONE', *, *, #4044, .T. ) ;
#49242=EDGE_CURVE ( 'NONE', #147359, #48110, #250741, .T. ) ;
#49398=VECTOR ( 'NONE', #215752, 1000.000000000000000 ) ;
#49460=ORIENTED_EDGE ( 'NONE', *, *, #150054, .F. ) ;
#49510=EDGE_CURVE ( 'NONE', #129272, #49816, #178973, .T. ) ;
#49618=CARTESIAN_POINT ( 'NONE',  ( -16.94445028196807002, 9.992063609708893068, -87.89266982158160602 ) ) ;
#49659=ORIENTED_EDGE ( 'NONE', *, *, #252492, .T. ) ;
#49693=LINE ( 'NONE', #129237, #249775 ) ;
#49816=VERTEX_POINT ( 'NONE', #140767 ) ;
#49929=CARTESIAN_POINT ( 'NONE',  ( 20.09999999999999787, 9.750000000011137757, -79.65000000000004832 ) ) ;
#50137=EDGE_LOOP ( 'NONE', ( #257336, #75929, #51102, #168855 ) ) ;
#50201=CARTESIAN_POINT ( 'NONE',  ( -16.97683809663752186, 9.950000000011138823, -87.09763598180373378 ) ) ;
#50361=CARTESIAN_POINT ( 'NONE',  ( -12.48127053791145258, 9.376580978055097049, -84.62694624701198620 ) ) ;
#50522=CARTESIAN_POINT ( 'NONE',  ( -20.65000000000000568, 7.250000000011138646, -79.65000000000004832 ) ) ;
#50602=VECTOR ( 'NONE', #58627, 1000.000000000000000 ) ;
#50649=EDGE_LOOP ( 'NONE', ( #127073, #22998, #28770, #125222, #20350, #119768 ) ) ;
#50674=ORIENTED_EDGE ( 'NONE', *, *, #206794, .F. ) ;
#50730=VECTOR ( 'NONE', #254217, 999.9999999999998863 ) ;
#50756=EDGE_CURVE ( 'NONE', #66750, #155242, #216465, .T. ) ;
#50757=DIRECTION ( 'NONE',  ( -1.652117596168391700E-15, -1.000000000000000000, 0.000000000000000000 ) ) ;
#50793=DIRECTION ( 'NONE',  ( 1.000000000000000000, 0.000000000000000000, 0.000000000000000000 ) ) ;
#50974=EDGE_LOOP ( 'NONE', ( #187751, #210835, #59811 ) ) ;
#51096=ADVANCED_FACE ( 'NONE', ( #171964 ), #15433, .F. ) ;
#51102=ORIENTED_EDGE ( 'NONE', *, *, #235090, .T. ) ;
#51128=CARTESIAN_POINT ( 'NONE',  ( -18.40000000000000213, 5.650000000011139001, -87.85000000000003695 ) ) ;
#51322=ORIENTED_EDGE ( 'NONE', *, *, #145646, .T. ) ;
#51344=CARTESIAN_POINT ( 'NONE',  ( -15.75000000000000355, 9.850000000011133849, -83.75000000000004263 ) ) ;
#51373=VECTOR ( 'NONE', #238849, 1000.000000000000000 ) ;
#51435=EDGE_CURVE ( 'NONE', #66750, #218042, #24427, .T. ) ;
#51484=CARTESIAN_POINT ( 'NONE',  ( -17.27223548804523645, 10.34539739142215886, -78.36639382080713290 ) ) ;
#51508=CARTESIAN_POINT ( 'NONE',  ( -13.22483237240078324, 9.436674251854004325, -82.17686193099926584 ) ) ;
#51590=ORIENTED_EDGE ( 'NONE', *, *, #201517, .F. ) ;
#51665=CARTESIAN_POINT ( 'NONE',  ( 18.54999999999999716, 9.950000000011153034, -87.85000000000010800 ) ) ;
#51721=CARTESIAN_POINT ( 'NONE',  ( 20.73486653747088226, 7.250000000011182166, -79.65000000000004832 ) ) ;
#52056=ORIENTED_EDGE ( 'NONE', *, *, #87337, .T. ) ;
#52305=EDGE_LOOP ( 'NONE', ( #45692, #14766, #223588, #158990 ) ) ;
#52422=ORIENTED_EDGE ( 'NONE', *, *, #256211, .F. ) ;
#52636=FACE_OUTER_BOUND ( 'NONE', #191211, .T. ) ;
#52660=CARTESIAN_POINT ( 'NONE',  ( -16.94037747912386394, 10.01353938249748765, -79.55113095797554479 ) ) ;
#52784=CARTESIAN_POINT ( 'NONE',  ( -16.94107738177415357, 10.01423928514777728, -79.55000000000003979 ) ) ;
#52828=CARTESIAN_POINT ( 'NONE',  ( -17.01825945287481545, 9.950000000011138823, -87.75000000000005684 ) ) ;
#52869=VERTEX_POINT ( 'NONE', #54361 ) ;
#52947=CARTESIAN_POINT ( 'NONE',  ( -13.77083647240106323, 9.457410930301319851, -85.49991590874631697 ) ) ;
#53010=ORIENTED_EDGE ( 'NONE', *, *, #254803, .F. ) ;
#53067=DIRECTION ( 'NONE',  ( 1.186688945009010077E-16, -1.000000000000000000, -0.000000000000000000 ) ) ;
#53374=EDGE_LOOP ( 'NONE', ( #92161, #111697, #231889, #206327, #185586, #186783 ) ) ;
#53458=CARTESIAN_POINT ( 'NONE',  ( -18.34374000495059676, 11.47316190337362940, -91.25000000000005684 ) ) ;
#53545=AXIS2_PLACEMENT_3D ( 'NONE', #69535, #72099, #252000 ) ;
#53672=ORIENTED_EDGE ( 'NONE', *, *, #17484, .T. ) ;
#53715=ORIENTED_EDGE ( 'NONE', *, *, #2673, .F. ) ;
#53892=CARTESIAN_POINT ( 'NONE',  ( -21.65000000000000213, 7.250000000011138646, -79.65000000000004832 ) ) ;
#53920=AXIS2_PLACEMENT_3D ( 'NONE', #8697, #223869, #146897 ) ;
#53952=CARTESIAN_POINT ( 'NONE',  ( -16.93230518875208190, 10.00075036143099716, -79.57577834810155082 ) ) ;
#53971=ORIENTED_EDGE ( 'NONE', *, *, #11065, .F. ) ;
#54078=CARTESIAN_POINT ( 'NONE',  ( -18.37013991200266005, 11.49974761622312691, -76.20697698948293919 ) ) ;
#54136=CARTESIAN_POINT ( 'NONE',  ( -18.39999999999999858, 11.47316190337362762, -76.32594606680801519 ) ) ;
#54219=CARTESIAN_POINT ( 'NONE',  ( -18.35663730107557257, 11.47390742652235573, -76.25000000000004263 ) ) ;
#54264=CARTESIAN_POINT ( 'NONE',  ( 13.99999999999999822, 9.850000000011137402, -83.75000000000004263 ) ) ;
#54282=VERTEX_POINT ( 'NONE', #31997 ) ;
#54297=ORIENTED_EDGE ( 'NONE', *, *, #242328, .F. ) ;
#54361=CARTESIAN_POINT ( 'NONE',  ( -16.94107738177414291, 10.01423928514777373, -87.95000000000004547 ) ) ;
#54457=CARTESIAN_POINT ( 'NONE',  ( 20.27550659511089037, 9.216043722520002035, -79.65000000000004832 ) ) ;
#54638=FACE_OUTER_BOUND ( 'NONE', #110041, .T. ) ;
#54726=PLANE ( 'NONE',  #166537 ) ;
#54751=DIRECTION ( 'NONE',  ( 1.000000000000000000, 0.000000000000000000, 0.000000000000000000 ) ) ;
#54752=LINE ( 'NONE', #69217, #223305 ) ;
#54934=VECTOR ( 'NONE', #133430, 1000.000000000000000 ) ;
#54985=AXIS2_PLACEMENT_3D ( 'NONE', #166459, #84258, #185985 ) ;
#54996=AXIS2_PLACEMENT_3D ( 'NONE', #32916, #17178, #135804 ) ;
#55153=CARTESIAN_POINT ( 'NONE',  ( -16.83558968593864336, 9.950000000011137047, -79.66230518761653911 ) ) ;
#55236=ORIENTED_EDGE ( 'NONE', *, *, #130908, .F. ) ;
#55380=DIRECTION ( 'NONE',  ( 1.186688945009009831E-16, -1.000000000000000000, 0.000000000000000000 ) ) ;
#55465=CARTESIAN_POINT ( 'NONE',  ( -16.86578989773640913, 9.984809801269951990, -87.96466488662228755 ) ) ;
#55760=AXIS2_PLACEMENT_3D ( 'NONE', #82682, #241791, #162278 ) ;
#55876=AXIS2_PLACEMENT_3D ( 'NONE', #238688, #241278, #199595 ) ;
#55904=DIRECTION ( 'NONE',  ( 1.000000000000000000, 0.000000000000000000, 1.073024830501117725E-15 ) ) ;
#56027=CARTESIAN_POINT ( 'NONE',  ( 14.45963434102924161, 9.451541661396667848, -85.45387549883061240 ) ) ;
#56045=VERTEX_POINT ( 'NONE', #90080 ) ;
#56334=FACE_OUTER_BOUND ( 'NONE', #112903, .T. ) ;
#56604=LINE ( 'NONE', #177894, #20502 ) ;
#56801=CARTESIAN_POINT ( 'NONE',  ( -17.27223548804936826, 10.34539739143179560, -89.13360617919259710 ) ) ;
#56852=VECTOR ( 'NONE', #95488, 1000.000000000000000 ) ;
#56865=AXIS2_PLACEMENT_3D ( 'NONE', #165086, #5995, #69859 ) ;
#56911=CARTESIAN_POINT ( 'NONE',  ( -16.91049119928362998, 9.950000000011138823, -87.88172039319088924 ) ) ;
#57208=ORIENTED_EDGE ( 'NONE', *, *, #152927, .T. ) ;
#57209=ADVANCED_FACE ( 'NONE', ( #114306 ), #110453, .F. ) ;
#57320=CARTESIAN_POINT ( 'NONE',  ( 15.07585980824113925, 9.417632963117448242, -85.14894846573231746 ) ) ;
#58226=CARTESIAN_POINT ( 'NONE',  ( 23.24999999999999645, 11.75000000001113953, -79.65000000000004832 ) ) ;
#58347=PLANE ( 'NONE',  #142109 ) ;
#58407=CARTESIAN_POINT ( 'NONE',  ( 15.74999999999999645, 9.850000000011137402, -83.75000000000004263 ) ) ;
#58430=ADVANCED_FACE ( 'NONE', ( #89972 ), #95884, .T. ) ;
#58569=CARTESIAN_POINT ( 'NONE',  ( 12.25000000000000000, 9.350000000011139178, -83.52151937182513564 ) ) ;
#58627=DIRECTION ( 'NONE',  ( -0.000000000000000000, -0.000000000000000000, -1.000000000000000000 ) ) ;
#58847=EDGE_CURVE ( 'NONE', #13912, #134549, #236548, .T. ) ;
#59004=CARTESIAN_POINT ( 'NONE',  ( -16.80891096016346253, 9.950000000011137047, -79.63233719273293332 ) ) ;
#59037=ADVANCED_FACE ( 'NONE', ( #124326 ), #103446, .F. ) ;
#59203=DIRECTION ( 'NONE',  ( 0.000000000000000000, -1.000000000000000000, 0.000000000000000000 ) ) ;
#59224=DIRECTION ( 'NONE',  ( -1.073024830501117725E-15, -0.000000000000000000, -1.000000000000000000 ) ) ;
#59373=AXIS2_PLACEMENT_3D ( 'NONE', #198796, #218342, #121848 ) ;
#59495=ORIENTED_EDGE ( 'NONE', *, *, #238093, .T. ) ;
#59523=VERTEX_POINT ( 'NONE', #255468 ) ;
#59560=CARTESIAN_POINT ( 'NONE',  ( -15.55912972643741199, 8.490870273573719373, -79.65000000000004832 ) ) ;
#59593=ORIENTED_EDGE ( 'NONE', *, *, #254803, .T. ) ;
#59811=ORIENTED_EDGE ( 'NONE', *, *, #49242, .F. ) ;
#60200=B_SPLINE_CURVE_WITH_KNOTS ( 'NONE', 3,
 ( #172942, #154647, #157214, #54219, #193747, #236703, #252413 ),
 .UNSPECIFIED., .F., .F.,
 ( 4, 3, 4 ),
 ( 0.000000000000000000, 4.520325912680675046E-05, 5.794988040901435228E-05 ),
 .UNSPECIFIED. ) ;
#60274=ORIENTED_EDGE ( 'NONE', *, *, #61366, .F. ) ;
#60279=CARTESIAN_POINT ( 'NONE',  ( -16.85312964099708211, 9.913604682078863917, -87.60281570643047644 ) ) ;
#60340=LINE ( 'NONE', #119055, #47725 ) ;
#60480=LINE ( 'NONE', #76194, #178920 ) ;
#60681=STYLED_ITEM ( 'NONE', ( #73955 ), #132074 ) ;
#60766=DIRECTION ( 'NONE',  ( -0.5932847527679310229, 0.8049926720990042694, -6.366092712777067056E-16 ) ) ;
#61366=EDGE_CURVE ( 'NONE', #23293, #189866, #122580, .T. ) ;
#61877=CARTESIAN_POINT ( 'NONE',  ( -16.96982749440706328, 9.950000000011137047, -87.37522159118832121 ) ) ;
#62105=ADVANCED_FACE ( 'NONE', ( #27989 ), #227635, .T. ) ;
#62166=DIRECTION ( 'NONE',  ( 0.000000000000000000, 0.000000000000000000, 1.000000000000000000 ) ) ;
#62309=ORIENTED_EDGE ( 'NONE', *, *, #14549, .T. ) ;
#62704=ORIENTED_EDGE ( 'NONE', *, *, #96656, .T. ) ;
#62847=CARTESIAN_POINT ( 'NONE',  ( 20.27550659511088682, 9.216043722520002035, -76.25000000000004263 ) ) ;
#63183=ORIENTED_EDGE ( 'NONE', *, *, #162245, .T. ) ;
#63761=DIRECTION ( 'NONE',  ( 1.186688945009010077E-16, -1.000000000000000000, -0.000000000000000000 ) ) ;
#63794=CARTESIAN_POINT ( 'NONE',  ( -16.27683809663750480, 9.350000000011133849, -87.95000000000004547 ) ) ;
#63823=CARTESIAN_POINT ( 'NONE',  ( -17.29158576265543346, 10.36474766602906783, -89.08275824479223104 ) ) ;
#63865=ORIENTED_EDGE ( 'NONE', *, *, #96656, .F. ) ;
#63876=DIRECTION ( 'NONE',  ( 0.000000000000000000, -1.000000000000000000, 0.000000000000000000 ) ) ;
#63911=CARTESIAN_POINT ( 'NONE',  ( -16.87851181299898684, 9.950042924018893231, -79.64985648463313339 ) ) ;
#64041=CARTESIAN_POINT ( 'NONE',  ( 20.27550659511089037, 9.216043722520002035, -87.85000000000003695 ) ) ;
#64121=DIRECTION ( 'NONE',  ( 0.000000000000000000, 0.000000000000000000, -1.000000000000000000 ) ) ;
#64281=CARTESIAN_POINT ( 'NONE',  ( -16.94225986326250322, 9.950000000011135270, -79.94671937560791264 ) ) ;
#64328=CIRCLE ( 'NONE', #114209, 14.30833333333333890 ) ;
#64545=ORIENTED_EDGE ( 'NONE', *, *, #227514, .F. ) ;
#64725=CARTESIAN_POINT ( 'NONE',  ( -16.86445178670638256, 9.962211629127160961, -87.89077743811738230 ) ) ;
#65128=CARTESIAN_POINT ( 'NONE',  ( -20.65000000000000568, 7.250000000011138646, -76.25000000000004263 ) ) ;
#65351=VERTEX_POINT ( 'NONE', #50522 ) ;
#65371=ADVANCED_FACE ( 'NONE', ( #133928 ), #107955, .F. ) ;
#65546=CYLINDRICAL_SURFACE ( 'NONE', #155519, 0.9000000000000014655 ) ;
#65556=ORIENTED_EDGE ( 'NONE', *, *, #245805, .T. ) ;
#65720=CARTESIAN_POINT ( 'NONE',  ( -16.84981964351497297, 9.917318234109998798, -87.63039838598058395 ) ) ;
#66111=ADVANCED_FACE ( 'NONE', ( #56334 ), #15978, .F. ) ;
#66179=CARTESIAN_POINT ( 'NONE',  ( 20.09999999999999787, 9.750000000011137757, -76.25000000000004263 ) ) ;
#66413=FACE_OUTER_BOUND ( 'NONE', #7534, .T. ) ;
#66500=EDGE_CURVE ( 'NONE', #176792, #108503, #252888, .T. ) ;
#66621=CARTESIAN_POINT ( 'NONE',  ( -16.93294127766158752, 10.00328010296601988, -87.92990726582927152 ) ) ;
#66636=DIRECTION ( 'NONE',  ( -0.000000000000000000, -0.000000000000000000, -1.000000000000000000 ) ) ;
#66642=AXIS2_PLACEMENT_3D ( 'NONE', #253047, #125722, #227393 ) ;
#66750=VERTEX_POINT ( 'NONE', #7296 ) ;
#67043=VERTEX_POINT ( 'NONE', #220890 ) ;
#67252=CARTESIAN_POINT ( 'NONE',  ( -16.87683809663752399, 9.850000000011144508, -80.40236401819635148 ) ) ;
#67286=ORIENTED_EDGE ( 'NONE', *, *, #90882, .F. ) ;
#67386=CARTESIAN_POINT ( 'NONE',  ( -15.51798037960204368, 9.376659938544690931, -84.62819254821734205 ) ) ;
#67653=FACE_OUTER_BOUND ( 'NONE', #147190, .T. ) ;
#67707=DIRECTION ( 'NONE',  ( -1.073024830501117725E-15, -0.000000000000000000, -1.000000000000000000 ) ) ;
#67759=CARTESIAN_POINT ( 'NONE',  ( -16.89060415895971090, 9.951220762813354881, -79.64592022427049756 ) ) ;
#67982=EDGE_CURVE ( 'NONE', #78107, #228775, #82406, .T. ) ;
#68009=LINE ( 'NONE', #6751, #217430 ) ;
#68262=EDGE_CURVE ( 'NONE', #143362, #112749, #154203, .T. ) ;
#68336=PLANE ( 'NONE',  #69233 ) ;
#68370=CARTESIAN_POINT ( 'NONE',  ( -17.11825945287482753, 10.05000000001113847, -79.65000000000004832 ) ) ;
#68408=AXIS2_PLACEMENT_3D ( 'NONE', #153379, #17657, #234143 ) ;
#68524=VERTEX_POINT ( 'NONE', #14174 ) ;
#68695=VECTOR ( 'NONE', #241236, 1000.000000000000000 ) ;
#69037=EDGE_CURVE ( 'NONE', #185121, #3745, #231611, .T. ) ;
#69211=CARTESIAN_POINT ( 'NONE',  ( -16.93433913041102912, 10.00597842153509376, -87.93536542739521167 ) ) ;
#69217=CARTESIAN_POINT ( 'NONE',  ( -21.64999999999999858, 9.350000000011133849, -87.85000000000003695 ) ) ;
#69233=AXIS2_PLACEMENT_3D ( 'NONE', #147880, #207867, #108739 ) ;
#69324=ORIENTED_EDGE ( 'NONE', *, *, #157483, .T. ) ;
#69535=CARTESIAN_POINT ( 'NONE',  ( -23.25000000000000355, 11.75000000001113953, -76.25000000000004263 ) ) ;
#69656=CARTESIAN_POINT ( 'NONE',  ( -16.85718274719422993, 9.976142314632891583, -79.56334633218253316 ) ) ;
#69691=CARTESIAN_POINT ( 'NONE',  ( -16.93909480342659890, 9.993078364812696179, -79.60034701667237300 ) ) ;
#69845=CARTESIAN_POINT ( 'NONE',  ( -12.84409460144753368, 9.410682294279109072, -82.43114344194833620 ) ) ;
#69859=DIRECTION ( 'NONE',  ( 0.7071067811865474617, 0.7071067811865474617, 0.000000000000000000 ) ) ;
#69941=CARTESIAN_POINT ( 'NONE',  ( -16.79814274880124358, 9.949272542688458287, -79.65243303704804134 ) ) ;
#69977=CARTESIAN_POINT ( 'NONE',  ( -12.60829076262180592, 9.389529397477891948, -84.81710791289371798 ) ) ;
#70013=CARTESIAN_POINT ( 'NONE',  ( -16.88328101497759448, 9.950352834230013599, -87.85117951492932775 ) ) ;
#70125=ORIENTED_EDGE ( 'NONE', *, *, #142531, .F. ) ;
#70466=CARTESIAN_POINT ( 'NONE',  ( -16.95709691156326215, 9.950000000011138823, -87.83994243749135933 ) ) ;
#70611=CARTESIAN_POINT ( 'NONE',  ( -18.40000000000000213, 11.48667500176882861, -91.25000000000005684 ) ) ;
#71255=B_SPLINE_CURVE_WITH_KNOTS ( 'NONE', 3,
 ( #71261, #251135, #188608, #231607, #8698, #171660, #50361, #69977, #149515, #191214, #246029, #206898, #52947, #27005, #111644, #89499, #247293, #9980, #129912, #186053, #7399, #249874, #11270, #67386, #86920, #166516, #167801, #209459, #169094, #248589 ),
 .UNSPECIFIED., .F., .F.,
 ( 4, 2, 2, 2, 2, 2, 2, 2, 2, 2, 2, 2, 2, 2, 4 ),
 ( 0.000000000000000000, 0.0003422764154113355664, 0.0006845528308226711328, 0.001026829246234006862, 0.001369105661645342266, 0.002053658492468009387, 0.002738211323290676725, 0.003080487738702010828, 0.003422764154113344063, 0.003765040569524678166, 0.004107316984936011835, 0.004449593400347345504, 0.004791869815758679173, 0.005134146231170016311, 0.005476422646581353450 ),
 .UNSPECIFIED. ) ;
#71256=CARTESIAN_POINT ( 'NONE',  ( 23.04999999999999716, 8.822561741677553471, -87.85000000000003695 ) ) ;
#71261=CARTESIAN_POINT ( 'NONE',  ( -12.25000000000000178, 9.350000000011139178, -83.75000000000004263 ) ) ;
#71575=VERTEX_POINT ( 'NONE', #192240 ) ;
#71748=ORIENTED_EDGE ( 'NONE', *, *, #136889, .T. ) ;
#71996=ORIENTED_EDGE ( 'NONE', *, *, #245974, .F. ) ;
#72099=DIRECTION ( 'NONE',  ( 0.000000000000000000, -1.000000000000000000, 0.000000000000000000 ) ) ;
#72172=B_SPLINE_CURVE_WITH_KNOTS ( 'NONE', 3,
 ( #20247, #97151, #120644, #198866, #159752, #16402, #137589, #195039, #55465, #239287 ),
 .UNSPECIFIED., .F., .F.,
 ( 4, 3, 3, 4 ),
 ( 7.632826238681696029E-06, 4.756916949875625587E-05, 9.484459048150268483E-05, 0.0001435500935099809469 ),
 .UNSPECIFIED. ) ;
#72371=CARTESIAN_POINT ( 'NONE',  ( -16.92989507731676113, 9.950000000011135270, -87.61749893061021055 ) ) ;
#72655=EDGE_LOOP ( 'NONE', ( #96325, #189651, #100486 ) ) ;
#72719=VERTEX_POINT ( 'NONE', #81570 ) ;
#72802=DIRECTION ( 'NONE',  ( 1.186688945009009831E-16, -1.000000000000000000, 0.000000000000000000 ) ) ;
#72856=CARTESIAN_POINT ( 'NONE',  ( -16.87683809663752399, 21.23804903844422043, -79.65000000000004832 ) ) ;
#72920=FACE_OUTER_BOUND ( 'NONE', #254478, .T. ) ;
#73486=LINE ( 'NONE', #53892, #54934 ) ;
#73955=PRESENTATION_STYLE_ASSIGNMENT (( #17776 ) ) ;
#73958=VERTEX_POINT ( 'NONE', #252589 ) ;
#74064=VERTEX_POINT ( 'NONE', #202577 ) ;
#74088=CARTESIAN_POINT ( 'NONE',  ( 20.73486653747088582, 7.250000000011182166, -87.85000000000003695 ) ) ;
#74185=EDGE_LOOP ( 'NONE', ( #175621, #49460, #234039, #219681, #136887, #176495, #51322, #104742, #169265, #53010, #54297, #156561 ) ) ;
#74206=EDGE_CURVE ( 'NONE', #222707, #23293, #18040, .T. ) ;
#74269=DIRECTION ( 'NONE',  ( -1.073024830501117725E-15, 0.000000000000000000, 1.000000000000000000 ) ) ;
#74354=CARTESIAN_POINT ( 'NONE',  ( 21.72449340488910607, 10.28395627750226815, -87.85000000000003695 ) ) ;
#74380=CARTESIAN_POINT ( 'NONE',  ( 13.22461703343585171, 9.436662931810239741, -85.32303673229492347 ) ) ;
#74619=EDGE_CURVE ( 'NONE', #102037, #41600, #48463, .T. ) ;
#74642=ORIENTED_EDGE ( 'NONE', *, *, #254482, .T. ) ;
#74816=CARTESIAN_POINT ( 'NONE',  ( -16.87036670365549895, 9.989418819312803066, -79.52043988269799968 ) ) ;
#75039=AXIS2_PLACEMENT_3D ( 'NONE', #72856, #170692, #251454 ) ;
#75069=CARTESIAN_POINT ( 'NONE',  ( -16.83199318825829138, 9.930646127992318384, -87.72758518820923257 ) ) ;
#75645=CARTESIAN_POINT ( 'NONE',  ( 12.68104795156993880, 9.396533993965071829, -84.90593977917332325 ) ) ;
#75929=ORIENTED_EDGE ( 'NONE', *, *, #99325, .F. ) ;
#76034=CARTESIAN_POINT ( 'NONE',  ( -16.88705144915408951, 9.950000000011138823, -79.93097859471261302 ) ) ;
#76052=CARTESIAN_POINT ( 'NONE',  ( -16.89318236219975589, 9.951535257886289898, -79.64487036789418539 ) ) ;
#76179=CARTESIAN_POINT ( 'NONE',  ( 16.87683809663749557, 9.950000000011131718, -87.85000000000005116 ) ) ;
#76194=CARTESIAN_POINT ( 'NONE',  ( -15.55912972643740488, 8.490870273573721150, -87.85000000000003695 ) ) ;
#76255=DIRECTION ( 'NONE',  ( 1.000000000000000000, 0.000000000000000000, 0.000000000000000000 ) ) ;
#76714=VECTOR ( 'NONE', #188690, 1000.000000000000000 ) ;
#76811=ORIENTED_EDGE ( 'NONE', *, *, #183439, .F. ) ;
#77128=VERTEX_POINT ( 'NONE', #46940 ) ;
#77307=CARTESIAN_POINT ( 'NONE',  ( -16.87683809663750978, 9.950000000011137047, -80.40236401819653622 ) ) ;
#77454=LINE ( 'NONE', #236546, #170848 ) ;
#77660=FACE_OUTER_BOUND ( 'NONE', #151465, .T. ) ;
#77819=CARTESIAN_POINT ( 'NONE',  ( -16.87845715379269507, 9.957858113908168107, -79.62380065105894289 ) ) ;
#78107=VERTEX_POINT ( 'NONE', #17365 ) ;
#78592=CARTESIAN_POINT ( 'NONE',  ( -16.93710578446423654, 9.950000000011137047, -79.91880398379943529 ) ) ;
#79025=ORIENTED_EDGE ( 'NONE', *, *, #230278, .F. ) ;
#79415=CARTESIAN_POINT ( 'NONE',  ( -17.22361732159831504, 10.34515565861358866, -89.12921547413290568 ) ) ;
#79507=EDGE_CURVE ( 'NONE', #187000, #236168, #172520, .T. ) ;
#79617=ORIENTED_EDGE ( 'NONE', *, *, #80881, .T. ) ;
#79839=CARTESIAN_POINT ( 'NONE',  ( -16.27683809663751191, 9.350000000011132073, -79.55000000000005400 ) ) ;
#80212=CARTESIAN_POINT ( 'NONE',  ( -16.94107738177414291, 10.01423928514777373, -87.95000000000004547 ) ) ;
#80225=ADVANCED_FACE ( 'NONE', ( #29816 ), #162897, .F. ) ;
#80253=EDGE_LOOP ( 'NONE', ( #70125, #6793, #87415, #44342, #82050, #199923, #151507, #94155, #188469, #40202, #156050, #103578, #110837, #81543 ) ) ;
#80700=CARTESIAN_POINT ( 'NONE',  ( 13.76927104934456558, 9.455987233623895705, -82.01153116689783928 ) ) ;
#80881=EDGE_CURVE ( 'NONE', #77128, #189866, #145092, .T. ) ;
#81003=CARTESIAN_POINT ( 'NONE',  ( -16.89268316805465986, 9.951721813253337601, -87.85575247854558256 ) ) ;
#81147=CARTESIAN_POINT ( 'NONE',  ( -16.83233564386401682, 9.930221796595741779, -79.77547933652442680 ) ) ;
#81543=ORIENTED_EDGE ( 'NONE', *, *, #137946, .T. ) ;
#81570=CARTESIAN_POINT ( 'NONE',  ( 21.13736287352038445, 8.046642376395153562, -79.65000000000004832 ) ) ;
#81779=VERTEX_POINT ( 'NONE', #222532 ) ;
#81884=CARTESIAN_POINT ( 'NONE',  ( 13.99999999999999822, 9.850000000011137402, -83.75000000000004263 ) ) ;
#81960=PLANE ( 'NONE',  #221677 ) ;
#82050=ORIENTED_EDGE ( 'NONE', *, *, #192, .F. ) ;
#82165=EDGE_LOOP ( 'NONE', ( #83843, #163027, #154259 ) ) ;
#82388=CARTESIAN_POINT ( 'NONE',  ( -16.80100914604134132, 9.943149094114721365, -87.81704412728768716 ) ) ;
#82406=LINE ( 'NONE', #162001, #211378 ) ;
#82682=CARTESIAN_POINT ( 'NONE',  ( 23.24999999999999645, 11.75000000001113953, -76.25000000000004263 ) ) ;
#82807=EDGE_CURVE ( 'NONE', #42422, #177843, #134381, .T. ) ;
#82997=PRODUCT_DEFINITION_SHAPE ( 'NONE', 'NONE',  #99334 ) ;
#83145=CARTESIAN_POINT ( 'NONE',  ( -16.87683809663752399, 9.850000000011140955, -79.65000000000004832 ) ) ;
#83257=CARTESIAN_POINT ( 'NONE',  ( 15.39793903038208001, 9.389686005666810331, -82.67284350635134160 ) ) ;
#83288=( BOUNDED_SURFACE ( )  B_SPLINE_SURFACE ( 3, 2, ( 
 ( #177735, #77307, #257182 ),
 ( #40791, #194726, #214266 ),
 ( #137281, #16094, #159441 ),
 ( #78592, #76034, #195998 ),
 ( #18628, #238971, #158188 ),
 ( #235117, #98128, #81147 ),
 ( #215538, #39513, #237679 ),
 ( #55153, #36949, #100692 ),
 ( #59004, #155612, #236388 ),
 ( #216817, #115164, #197264 ) ),
 .UNSPECIFIED., .F., .F., .F. ) 
 B_SPLINE_SURFACE_WITH_KNOTS ( ( 4, 2, 2, 2, 4 ),
 ( 3, 3 ),
 ( 0.002161241639767785133, 0.002579950749617447234, 0.002789305304542278284, 0.002893982582004694243, 0.002998659859467109768 ),
 ( 0.000000000000000000, 1.000000000000000000 ),
 .UNSPECIFIED. ) 
 GEOMETRIC_REPRESENTATION_ITEM ( )  RATIONAL_B_SPLINE_SURFACE ( (
 ( 1.000000000000000000, 0.7071067811864923947, 1.000000000000000000),
 ( 1.000000000000000000, 0.7632447400663529002, 1.000000000000000000),
 ( 1.000000000000000000, 0.8158073005109872655, 1.000000000000000000),
 ( 1.000000000000000000, 0.8906973462395572083, 1.000000000000000000),
 ( 1.000000000000000000, 0.9149408947799931857, 1.000000000000000000),
 ( 1.000000000000000000, 0.9493368785275779764, 1.000000000000000000),
 ( 1.000000000000000000, 0.9605194247155937060, 1.000000000000000000),
 ( 1.000000000000000000, 0.9803630264781856285, 1.000000000000000000),
 ( 1.000000000000000000, 0.9900844824270625955, 1.000000000000000000),
 ( 1.000000000000000000, 0.9894588281429246290, 1.000000000000000000) ) ) 
 REPRESENTATION_ITEM ( '' )  SURFACE ( )  );
#83411=ADVANCED_FACE ( 'NONE', ( #253405 ), #143075, .T. ) ;
#83524=DIRECTION ( 'NONE',  ( -1.000000000000000000, 0.000000000000000000, 1.073024830501117725E-15 ) ) ;
#83528=CARTESIAN_POINT ( 'NONE',  ( -16.77683809663752257, 9.945835743215301505, -79.66394901910425119 ) ) ;
#83827=B_SPLINE_CURVE_WITH_KNOTS ( 'NONE', 3,
 ( #47337, #185584, #145156, #142584, #8247, #244256, #4365, #87753, #27832, #128187 ),
 .UNSPECIFIED., .F., .F.,
 ( 4, 3, 3, 4 ),
 ( -2.000561356210515597E-06, 0.000000000000000000, 1.787822682428821068E-05, 4.206475347089863842E-05 ),
 .UNSPECIFIED. ) ;
#83843=ORIENTED_EDGE ( 'NONE', *, *, #188663, .T. ) ;
#83895=CARTESIAN_POINT ( 'NONE',  ( 18.39999999999999503, 11.47316190337363828, -79.65000000000004832 ) ) ;
#83948=CARTESIAN_POINT ( 'NONE',  ( -16.77431908686106610, 9.945805754529134290, -87.83583921765028890 ) ) ;
#83998=ADVANCED_FACE ( 'NONE', ( #239978 ), #5173, .F. ) ;
#84144=ORIENTED_EDGE ( 'NONE', *, *, #142531, .T. ) ;
#84258=DIRECTION ( 'NONE',  ( 1.000000000000000000, -0.000000000000000000, -0.000000000000000000 ) ) ;
#84415=LINE ( 'NONE', #164014, #183390 ) ;
#84563=ORIENTED_EDGE ( 'NONE', *, *, #74206, .F. ) ;
#84701=CARTESIAN_POINT ( 'NONE',  ( -23.25000000000000355, 5.650000000011139001, -76.25000000000004263 ) ) ;
#84979=ADVANCED_FACE ( 'NONE', ( #6380 ), #87183, .F. ) ;
#85038=ADVANCED_FACE ( 'NONE', ( #243713 ), #127622, .F. ) ;
#85247=CARTESIAN_POINT ( 'NONE',  ( -16.97683809663752186, 9.950000000011137047, -87.09763598180373378 ) ) ;
#85300=DIRECTION ( 'NONE',  ( 1.186688945009010077E-16, -1.000000000000000000, -0.000000000000000000 ) ) ;
#85315=CARTESIAN_POINT ( 'NONE',  ( 18.39999999999997371, 11.47316190337362940, -91.25000000000005684 ) ) ;
#85535=CARTESIAN_POINT ( 'NONE',  ( -16.87036670365548474, 9.989418819312801290, -87.97956011730209980 ) ) ;
#86286=DIRECTION ( 'NONE',  ( -1.000000000000000000, -0.000000000000000000, -0.000000000000000000 ) ) ;
#86493=DIRECTION ( 'NONE',  ( -0.000000000000000000, -0.000000000000000000, -1.000000000000000000 ) ) ;
#86608=( NAMED_UNIT ( * ) PLANE_ANGLE_UNIT ( ) SI_UNIT ( $, .RADIAN. ) );
#86786=EDGE_LOOP ( 'NONE', ( #62309, #130754 ) ) ;
#86811=FACE_OUTER_BOUND ( 'NONE', #100284, .T. ) ;
#86820=ORIENTED_EDGE ( 'NONE', *, *, #90882, .T. ) ;
#86920=CARTESIAN_POINT ( 'NONE',  ( -15.57281606413133979, 9.370655051134635372, -84.52582325598092439 ) ) ;
#86927=AXIS2_PLACEMENT_3D ( 'NONE', #166848, #67707, #128977 ) ;
#87038=( LENGTH_UNIT ( ) NAMED_UNIT ( * ) SI_UNIT ( .MILLI., .METRE. ) );
#87104=CARTESIAN_POINT ( 'NONE',  ( -14.00000000000000178, 9.850000000011133849, -83.75000000000004263 ) ) ;
#87183=PLANE ( 'NONE',  #154767 ) ;
#87204=LINE ( 'NONE', #213247, #4856 ) ;
#87293=CARTESIAN_POINT ( 'NONE',  ( -18.40000000000000213, 5.650000000011139001, -79.65000000000004832 ) ) ;
#87337=EDGE_CURVE ( 'NONE', #241566, #8126, #83827, .T. ) ;
#87415=ORIENTED_EDGE ( 'NONE', *, *, #238036, .F. ) ;
#87448=CARTESIAN_POINT ( 'NONE',  ( -16.93344882324368683, 9.996588767299030565, -87.91302569480497198 ) ) ;
#87551=ORIENTED_EDGE ( 'NONE', *, *, #203800, .T. ) ;
#87597=EDGE_CURVE ( 'NONE', #172515, #147359, #211580, .T. ) ;
#87753=CARTESIAN_POINT ( 'NONE',  ( -16.80117486205003630, 9.949657268323468529, -87.84885487292552853 ) ) ;
#87806=ORIENTED_EDGE ( 'NONE', *, *, #91931, .F. ) ;
#87862=EDGE_LOOP ( 'NONE', ( #46902, #174677, #79025, #121362 ) ) ;
#87893=EDGE_CURVE ( 'NONE', #242585, #134549, #54752, .T. ) ;
#87895=CARTESIAN_POINT ( 'NONE',  ( -16.92209698673727303, 9.950000000011138823, -79.71063556705212250 ) ) ;
#87922=DIRECTION ( 'NONE',  ( -0.000000000000000000, -0.000000000000000000, -1.000000000000000000 ) ) ;
#88016=CARTESIAN_POINT ( 'NONE',  ( 12.25000000000000000, 9.850000000011137402, -83.75000000000004263 ) ) ;
#88050=ADVANCED_FACE ( 'NONE', ( #86811 ), #244613, .F. ) ;
#88108=CARTESIAN_POINT ( 'NONE',  ( -16.92973740335348509, 9.992503814478576274, -87.90605903520246045 ) ) ;
#88280=DIRECTION ( 'NONE',  ( -1.000000000000000000, -1.646408749285562691E-14, 1.073024830501117725E-15 ) ) ;
#88362=DIRECTION ( 'NONE',  ( -1.020425574104004196E-15, 0.000000000000000000, 1.000000000000000000 ) ) ;
#88573=DIRECTION ( 'NONE',  ( -1.000000000000000000, 0.000000000000000000, 0.000000000000000000 ) ) ;
#88722=CARTESIAN_POINT ( 'NONE',  ( -16.94107738177414291, 10.01423928514777373, -87.95000000000004547 ) ) ;
#88791=ADVANCED_FACE ( 'NONE', ( #54638 ), #235844, .F. ) ;
#89191=CARTESIAN_POINT ( 'NONE',  ( -16.92778301347272674, 10.00094491684634868, -79.57148189203122968 ) ) ;
#89200=CARTESIAN_POINT ( 'NONE',  ( -17.04295772865440028, 10.02489942527099842, -79.65000000000004832 ) ) ;
#89224=CARTESIAN_POINT ( 'NONE',  ( -16.94107738177415712, 10.01423928514777728, -79.55000000000005400 ) ) ;
#89366=CARTESIAN_POINT ( 'NONE',  ( -12.60206096961791822, 9.389686005666813884, -82.67284350635138424 ) ) ;
#89499=CARTESIAN_POINT ( 'NONE',  ( -14.45422546970483957, 9.450602096099682825, -85.44389596309675028 ) ) ;
#89503=EDGE_CURVE ( 'NONE', #3167, #236242, #64328, .T. ) ;
#89535=CARTESIAN_POINT ( 'NONE',  ( -16.87665923198281348, 9.950000000011138823, -87.85000000000005116 ) ) ;
#89972=FACE_OUTER_BOUND ( 'NONE', #140282, .T. ) ;
#90080=CARTESIAN_POINT ( 'NONE',  ( -17.11825945287481332, 9.950000000011138823, -87.75000000000005684 ) ) ;
#90119=CARTESIAN_POINT ( 'NONE',  ( -18.38817693311004575, 11.48149151591092476, -91.25000000000005684 ) ) ;
#90163=EDGE_LOOP ( 'NONE', ( #137920, #87551, #165855, #224633 ) ) ;
#90462=ORIENTED_EDGE ( 'NONE', *, *, #153315, .F. ) ;
#90495=EDGE_LOOP ( 'NONE', ( #104234, #183314, #176902, #27365 ) ) ;
#90841=ADVANCED_FACE ( 'NONE', ( #175484 ), #231599, .F. ) ;
#90882=EDGE_CURVE ( 'NONE', #214712, #108130, #60200, .T. ) ;
#90973=CARTESIAN_POINT ( 'NONE',  ( 20.99999999999999645, 9.750000000011137757, -79.65000000000004832 ) ) ;
#91072=CARTESIAN_POINT ( 'NONE',  ( -18.40000000000000213, 11.47867410001105881, -91.22530678365944823 ) ) ;
#91158=LINE ( 'NONE', #87293, #198385 ) ;
#91282=CARTESIAN_POINT ( 'NONE',  ( -17.04295772865488345, 10.02489942527116007, -87.85000000000003695 ) ) ;
#91308=EDGE_CURVE ( 'NONE', #130466, #203569, #205942, .T. ) ;
#91326=EDGE_CURVE ( 'NONE', #170888, #3167, #21261, .T. ) ;
#91335=ORIENTED_EDGE ( 'NONE', *, *, #117763, .F. ) ;
#91337=EDGE_CURVE ( 'NONE', #185693, #236168, #60340, .T. ) ;
#91344=CIRCLE ( 'NONE', #220342, 0.09999999999999939493 ) ;
#91583=CIRCLE ( 'NONE', #66642, 0.09999999999999939493 ) ;
#91866=FACE_OUTER_BOUND ( 'NONE', #200327, .T. ) ;
#91931=EDGE_CURVE ( 'NONE', #143848, #17316, #152854, .T. ) ;
#91947=CARTESIAN_POINT ( 'NONE',  ( -15.75000000000000711, 9.350000000011140955, -83.52151937182513564 ) ) ;
#92071=DIRECTION ( 'NONE',  ( -1.073024830501117725E-15, 0.000000000000000000, 1.000000000000000000 ) ) ;
#92161=ORIENTED_EDGE ( 'NONE', *, *, #107824, .T. ) ;
#92192=FACE_OUTER_BOUND ( 'NONE', #50137, .T. ) ;
#92250=CARTESIAN_POINT ( 'NONE',  ( -16.87683809663752399, 9.950000000011142376, -79.65000000000004832 ) ) ;
#92346=CARTESIAN_POINT ( 'NONE',  ( -18.40000000000000213, 11.47316190337310893, -91.20017075153431563 ) ) ;
#92599=CARTESIAN_POINT ( 'NONE',  ( 12.48201962039796520, 9.376659938544690931, -84.62819254821734205 ) ) ;
#92739=( BOUNDED_SURFACE ( )  B_SPLINE_SURFACE ( 3, 2, ( 
 ( #151930, #209299, #54078 ),
 ( #31980, #232741, #230152 ),
 ( #189745, #51484, #153221 ),
 ( #52784, #93202, #172796 ) ),
 .UNSPECIFIED., .F., .F., .F. ) 
 B_SPLINE_SURFACE_WITH_KNOTS ( ( 4, 4 ),
 ( 3, 3 ),
 ( 5.727910411845712702, 5.983100554402349225 ),
 ( 0.000000000000000000, 1.000000000000000000 ),
 .UNSPECIFIED. ) 
 GEOMETRIC_REPRESENTATION_ITEM ( )  RATIONAL_B_SPLINE_SURFACE ( (
 ( 1.000000000000000000, 0.8946697475932183785, 1.000000000000000000),
 ( 1.000000000000000000, 0.9035312726220551260, 1.000000000000000000),
 ( 1.000000000000000000, 0.9104333467450264061, 1.000000000000000000),
 ( 1.000000000000000000, 0.9152888060719349683, 1.000000000000000000) ) ) 
 REPRESENTATION_ITEM ( '' )  SURFACE ( )  );
#93202=CARTESIAN_POINT ( 'NONE',  ( -16.91256925476570672, 9.985731158139332209, -79.53235751099475692 ) ) ;
#93226=CARTESIAN_POINT ( 'NONE',  ( -12.47155713865592475, 9.375669526436929857, -82.86779000938599893 ) ) ;
#93384=CARTESIAN_POINT ( 'NONE',  ( -16.91247567987037925, 9.959082683680399839, -79.62872445853739123 ) ) ;
#93654=CARTESIAN_POINT ( 'NONE',  ( 18.39999999999997371, 11.75000000001113953, -76.25000000000004263 ) ) ;
#93719=ORIENTED_EDGE ( 'NONE', *, *, #68262, .F. ) ;
#93895=CARTESIAN_POINT ( 'NONE',  ( 15.31784899511109899, 9.396630376328872103, -84.90705739281834497 ) ) ;
#93979=CARTESIAN_POINT ( 'NONE',  ( -18.38204789744325396, 11.47950103717623982, -91.25000000000005684 ) ) ;
#94009=CARTESIAN_POINT ( 'NONE',  ( -18.39999999999999858, 11.75000000001113953, -76.25000000000004263 ) ) ;
#94155=ORIENTED_EDGE ( 'NONE', *, *, #66500, .F. ) ;
#94325=CARTESIAN_POINT ( 'NONE',  ( -16.94107738177415712, 10.01423928514777550, -79.55000000000005400 ) ) ;
#94545=CARTESIAN_POINT ( 'NONE',  ( -18.39999999999999858, 11.47316190337362762, -76.29982924846605385 ) ) ;
#94551=CARTESIAN_POINT ( 'NONE',  ( -15.55912972643740488, 8.490870273573721150, -87.95000000000004547 ) ) ;
#94824=CARTESIAN_POINT ( 'NONE',  ( -16.86578989773641979, 9.984809801269951990, -79.53533511337781192 ) ) ;
#95187=CARTESIAN_POINT ( 'NONE',  ( 12.60873083341396850, 9.389571634557563939, -84.81764071236919733 ) ) ;
#95315=AXIS2_PLACEMENT_3D ( 'NONE', #104402, #183967, #5295 ) ;
#95407=AXIS2_PLACEMENT_3D ( 'NONE', #168394, #72802, #147494 ) ;
#95488=DIRECTION ( 'NONE',  ( 1.000000000000000000, 0.000000000000000000, 1.073024830501117725E-15 ) ) ;
#95741=DIRECTION ( 'NONE',  ( 1.000000000000000000, -0.000000000000000000, -0.000000000000000000 ) ) ;
#95793=B_SPLINE_CURVE_WITH_KNOTS ( 'NONE', 3,
 ( #152624, #191754, #112207, #215134, #13098, #230867, #114754, #135578, #93895, #57320, #155195, #56027, #35247, #194315, #234700, #254238, #131742, #74380, #15681, #195595, #170927, #75645, #95187, #92599, #172208, #153932, #174775, #173498, #232145, #116052 ),
 .UNSPECIFIED., .F., .F.,
 ( 4, 2, 2, 2, 2, 2, 2, 2, 2, 2, 2, 2, 2, 2, 4 ),
 ( 0.000000000000000000, 0.0003422764154113348617, 0.0006845528308226697233, 0.001026829246234006428, 0.001369105661645343350, 0.002053658492468013290, 0.002738211323290683664, 0.003080487738702016465, 0.003422764154113348400, 0.003765040569524680768, 0.004107316984936013569, 0.004449593400347345504, 0.004791869815758678305, 0.005134146231170010240, 0.005476422646581343041 ),
 .UNSPECIFIED. ) ;
#95884=( BOUNDED_SURFACE ( )  B_SPLINE_SURFACE ( 3, 2, ( 
 ( #30044, #56911, #169573 ),
 ( #136460, #70466, #37405 ),
 ( #149988, #17805, #91282 ),
 ( #196450, #97319, #246490 ) ),
 .UNSPECIFIED., .F., .F., .F. ) 
 B_SPLINE_SURFACE_WITH_KNOTS ( ( 4, 4 ),
 ( 3, 3 ),
 ( 3.658908243880847788, 4.712388980384689674 ),
 ( 0.000000000000000000, 1.000000000000000000 ),
 .UNSPECIFIED. ) 
 GEOMETRIC_REPRESENTATION_ITEM ( )  RATIONAL_B_SPLINE_SURFACE ( (
 ( 1.000000000000000000, 0.8984936768950610997, 1.000000000000000000),
 ( 1.000000000000000000, 0.8646876308615627504, 1.000000000000000000),
 ( 1.000000000000000000, 0.7953136715913320387, 1.000000000000000000),
 ( 1.000000000000000000, 0.7071067811865475727, 1.000000000000000000) ) ) 
 REPRESENTATION_ITEM ( '' )  SURFACE ( )  );
#96068=AXIS2_PLACEMENT_3D ( 'NONE', #87104, #106658, #105359 ) ;
#96148=DIRECTION ( 'NONE',  ( 0.000000000000000000, 1.000000000000000000, 0.000000000000000000 ) ) ;
#96163=PLANE ( 'NONE',  #95407 ) ;
#96244=FACE_OUTER_BOUND ( 'NONE', #114131, .T. ) ;
#96316=DIRECTION ( 'NONE',  ( 1.000000000000000000, 0.000000000000000000, 0.000000000000000000 ) ) ;
#96325=ORIENTED_EDGE ( 'NONE', *, *, #203800, .F. ) ;
#96453=DIRECTION ( 'NONE',  ( 1.000000000000000000, 0.000000000000000000, 0.000000000000000000 ) ) ;
#96519=DIRECTION ( 'NONE',  ( -1.000000000000000000, 0.000000000000000000, 0.000000000000000000 ) ) ;
#96656=EDGE_CURVE ( 'NONE', #134584, #45686, #247702, .T. ) ;
#96995=EDGE_CURVE ( 'NONE', #59523, #71575, #84415, .T. ) ;
#97087=DIRECTION ( 'NONE',  ( -0.7071067811865456854, 0.7071067811865493491, 0.000000000000000000 ) ) ;
#97151=CARTESIAN_POINT ( 'NONE',  ( -16.88460203013675454, 9.954759003246872240, -87.86589180953826883 ) ) ;
#97319=CARTESIAN_POINT ( 'NONE',  ( -17.11825945287481687, 9.950000000011140600, -87.85000000000005116 ) ) ;
#97360=CARTESIAN_POINT ( 'NONE',  ( -16.86379686415369861, 9.975217759264314310, -79.56661011090976388 ) ) ;
#97884=VERTEX_POINT ( 'NONE', #112108 ) ;
#98128=CARTESIAN_POINT ( 'NONE',  ( -16.85722902420149794, 9.950000000011137047, -79.76554747377056742 ) ) ;
#98156=CARTESIAN_POINT ( 'NONE',  ( 18.54999999999999716, 8.750000000011182166, -79.65000000000004832 ) ) ;
#98364=DIRECTION ( 'NONE',  ( -0.7071067811865562325, -0.7071067811865388020, 0.000000000000000000 ) ) ;
#98484=CARTESIAN_POINT ( 'NONE',  ( -16.89268316805465986, 9.951721813253337601, -87.85575247854558256 ) ) ;
#99032=CLOSED_SHELL ( 'NONE', ( #15735, #204484, #251805, #200662, #41063, #222422, #42779, #222960, #148939, #84979, #57209, #26768, #203980, #83998, #85038, #144639, #226004, #59037, #129098, #33929, #90841, #189899, #232265, #135346, #66111, #166297, #88791, #169745, #3979, #200432, #170401, #65371, #248033, #175318, #143079, #177061, #80225, #51096, #248923, #39564, #100860, #13383, #251017, #88050, #44585, #226551, #83411, #230922, #62105, #164540, #234010, #58430, #110142 ) ) ;
#99325=EDGE_CURVE ( 'NONE', #181633, #103997, #233488, .T. ) ;
#99334=PRODUCT_DEFINITION ( 'UNKNOWN', '', #173906, #131903 ) ;
#99443=CYLINDRICAL_SURFACE ( 'NONE', #157147, 0.5000000000000004441 ) ;
#99446=CARTESIAN_POINT ( 'NONE',  ( -16.90202395485713893, 9.965944544561935459, -79.59698627874068677 ) ) ;
#99547=DIRECTION ( 'NONE',  ( 0.000000000000000000, 0.000000000000000000, 1.000000000000000000 ) ) ;
#99631=ORIENTED_EDGE ( 'NONE', *, *, #91308, .T. ) ;
#99844=VECTOR ( 'NONE', #203252, 1000.000000000000000 ) ;
#100284=EDGE_LOOP ( 'NONE', ( #253892, #53672, #23008, #188167, #216365 ) ) ;
#100364=LINE ( 'NONE', #182524, #178257 ) ;
#100486=ORIENTED_EDGE ( 'NONE', *, *, #137946, .F. ) ;
#100692=CARTESIAN_POINT ( 'NONE',  ( -16.80621392010904103, 9.942202577518958861, -79.68959196541678125 ) ) ;
#100715=CARTESIAN_POINT ( 'NONE',  ( -16.94878442675511820, 9.991729103002155554, -79.61178042436216629 ) ) ;
#100722=DIRECTION ( 'NONE',  ( -0.000000000000000000, -0.000000000000000000, -1.000000000000000000 ) ) ;
#100782=FACE_OUTER_BOUND ( 'NONE', #213439, .T. ) ;
#100851=DIRECTION ( 'NONE',  ( -1.000000000000000000, 0.000000000000000000, -0.000000000000000000 ) ) ;
#100860=ADVANCED_FACE ( 'NONE', ( #21480 ), #116460, .F. ) ;
#101053=ORIENTED_EDGE ( 'NONE', *, *, #257021, .F. ) ;
#101332=CARTESIAN_POINT ( 'NONE',  ( -18.40000000000000213, 11.33174054713633261, -87.85000000000003695 ) ) ;
#101434=DIRECTION ( 'NONE',  ( 1.186688945009009831E-16, -1.000000000000000000, 0.000000000000000000 ) ) ;
#101463=ORIENTED_EDGE ( 'NONE', *, *, #221811, .F. ) ;
#101531=CARTESIAN_POINT ( 'NONE',  ( 14.22821877134046353, 9.456028260519072859, -82.01119803506577455 ) ) ;
#101589=FACE_OUTER_BOUND ( 'NONE', #7925, .T. ) ;
#101877=CARTESIAN_POINT ( 'NONE',  ( 20.05000000000002913, 7.250000000011171508, -76.25000000000004263 ) ) ;
#101930=CARTESIAN_POINT ( 'NONE',  ( -17.11825945287482753, 10.05000000001113847, -79.75000000000004263 ) ) ;
#102015=CARTESIAN_POINT ( 'NONE',  ( -16.87683809663752754, 9.864913778549567525, -80.27571563563854795 ) ) ;
#102037=VERTEX_POINT ( 'NONE', #93654 ) ;
#102185=ORIENTED_EDGE ( 'NONE', *, *, #17484, .F. ) ;
#102420=VECTOR ( 'NONE', #88280, 1000.000000000000000 ) ;
#102427=ORIENTED_EDGE ( 'NONE', *, *, #212464, .F. ) ;
#102449=CARTESIAN_POINT ( 'NONE',  ( 18.54999999999999716, 8.750000000011173285, -79.65000000000004832 ) ) ;
#102638=CARTESIAN_POINT ( 'NONE',  ( -16.94107738177415712, 10.01423928514777728, -79.55000000000005400 ) ) ;
#102764=VERTEX_POINT ( 'NONE', #217780 ) ;
#102827=CARTESIAN_POINT ( 'NONE',  ( 13.88302573338718560, 9.457410944778565920, -82.00008397379008329 ) ) ;
#102887=CARTESIAN_POINT ( 'NONE',  ( -23.25000000000000355, 10.05000000001113847, -87.75000000000005684 ) ) ;
#102963=EDGE_CURVE ( 'NONE', #189866, #228775, #245069, .T. ) ;
#103136=CARTESIAN_POINT ( 'NONE',  ( -16.93935632781549572, 9.984730499736244269, -87.88966074871035516 ) ) ;
#103223=EDGE_LOOP ( 'NONE', ( #12296, #245723, #240050, #140917 ) ) ;
#103446=PLANE ( 'NONE',  #210996 ) ;
#103578=ORIENTED_EDGE ( 'NONE', *, *, #160744, .T. ) ;
#103753=CARTESIAN_POINT ( 'NONE',  ( 18.39999999999999503, 8.822561741677553471, -91.25000000000005684 ) ) ;
#103808=CARTESIAN_POINT ( 'NONE',  ( 18.39999999999999503, 11.75000000001113953, -87.85000000000003695 ) ) ;
#103905=DIRECTION ( 'NONE',  ( 0.000000000000000000, 0.000000000000000000, 1.000000000000000000 ) ) ;
#103997=VERTEX_POINT ( 'NONE', #51344 ) ;
#104004=AXIS2_PLACEMENT_3D ( 'NONE', #253043, #18290, #96519 ) ;
#104234=ORIENTED_EDGE ( 'NONE', *, *, #23504, .T. ) ;
#104402=CARTESIAN_POINT ( 'NONE',  ( 20.27550659511088682, 9.216043722520002035, -76.25000000000004263 ) ) ;
#104482=CARTESIAN_POINT ( 'NONE',  ( -18.40000000000000213, 11.47316190337362940, -79.60857864376274051 ) ) ;
#104639=DIRECTION ( 'NONE',  ( 1.000000000000000000, 1.646408749285562691E-14, 1.073024830501117725E-15 ) ) ;
#104742=ORIENTED_EDGE ( 'NONE', *, *, #138212, .F. ) ;
#104991=LINE ( 'NONE', #88016, #150708 ) ;
#105329=EDGE_LOOP ( 'NONE', ( #164684, #167378, #123257, #168692, #253649, #37915, #64545, #166648, #15882, #146623 ) ) ;
#105359=DIRECTION ( 'NONE',  ( 1.000000000000000000, 0.000000000000000000, 0.000000000000000000 ) ) ;
#105366=CARTESIAN_POINT ( 'NONE',  ( -16.97683809663752186, 9.950000000011138823, -80.40236401819653622 ) ) ;
#105446=CARTESIAN_POINT ( 'NONE',  ( 16.27683809663750125, 9.350000000011137402, -76.25000000000004263 ) ) ;
#105565=CARTESIAN_POINT ( 'NONE',  ( -16.88560720703333473, 9.950564843760847822, -79.64811192086376934 ) ) ;
#105690=CARTESIAN_POINT ( 'NONE',  ( -16.93301857435212909, 9.976309354746613067, -87.88577557116147432 ) ) ;
#105794=LINE ( 'NONE', #62847, #192745 ) ;
#106658=DIRECTION ( 'NONE',  ( 1.186688945009009831E-16, -1.000000000000000000, 0.000000000000000000 ) ) ;
#106780=CARTESIAN_POINT ( 'NONE',  ( -21.65000000000000213, 7.250000000011139534, -87.85000000000003695 ) ) ;
#106892=ORIENTED_EDGE ( 'NONE', *, *, #120089, .F. ) ;
#107286=ORIENTED_EDGE ( 'NONE', *, *, #79507, .T. ) ;
#107352=CARTESIAN_POINT ( 'NONE',  ( -23.25000000000000355, 11.75000000001113953, -79.65000000000004832 ) ) ;
#107376=DIRECTION ( 'NONE',  ( 0.000000000000000000, 0.000000000000000000, -1.000000000000000000 ) ) ;
#107470=EDGE_CURVE ( 'NONE', #233341, #97884, #40320, .T. ) ;
#107497=CARTESIAN_POINT ( 'NONE',  ( -33.72168855820452649, 11.47316190337362940, -91.25000000000005684 ) ) ;
#107545=VECTOR ( 'NONE', #2519, 1000.000000000000000 ) ;
#107569=DIRECTION ( 'NONE',  ( 0.000000000000000000, 0.000000000000000000, 1.000000000000000000 ) ) ;
#107824=EDGE_CURVE ( 'NONE', #49816, #229007, #161213, .T. ) ;
#107854=ORIENTED_EDGE ( 'NONE', *, *, #177789, .F. ) ;
#107955=PLANE ( 'NONE',  #194104 ) ;
#108130=VERTEX_POINT ( 'NONE', #228882 ) ;
#108234=LINE ( 'NONE', #183911, #223604 ) ;
#108474=ORIENTED_EDGE ( 'NONE', *, *, #87597, .T. ) ;
#108503=VERTEX_POINT ( 'NONE', #49929 ) ;
#108509=ORIENTED_EDGE ( 'NONE', *, *, #180539, .F. ) ;
#108739=DIRECTION ( 'NONE',  ( -1.020425574104004196E-15, 0.000000000000000000, -1.000000000000000000 ) ) ;
#108789=CARTESIAN_POINT ( 'NONE',  ( -16.93339986808596720, 10.00510392857707664, -79.56599367181290461 ) ) ;
#108937=CARTESIAN_POINT ( 'NONE',  ( -13.43673303185028978, 9.446648990640015953, -82.08916329592322825 ) ) ;
#109141=CARTESIAN_POINT ( 'NONE',  ( -18.40000000000000213, 5.650000000011139001, -87.85000000000003695 ) ) ;
#109198=B_SPLINE_CURVE_WITH_KNOTS ( 'NONE', 3,
 ( #88722, #206131, #189133, #69211, #247822, #66621, #127881, #144855, #47030, #87448, #30086, #150027, #228270, #126591, #226975, #49618 ),
 .UNSPECIFIED., .F., .F.,
 ( 4, 3, 3, 3, 3, 4 ),
 ( 0.000000000000000000, 1.810570668009715449E-05, 2.740575833571675123E-05, 4.256816319436012815E-05, 5.213463471024871391E-05, 6.641585710718335726E-05 ),
 .UNSPECIFIED. ) ;
#109328=CARTESIAN_POINT ( 'NONE',  ( -18.40000000000000213, 11.47316190337364183, -91.17405393319209850 ) ) ;
#109564=VECTOR ( 'NONE', #210770, 999.9999999999998863 ) ;
#109871=CIRCLE ( 'NONE', #55876, 0.1000000000000001305 ) ;
#110041=EDGE_LOOP ( 'NONE', ( #186663, #292, #108474, #189121, #107286, #166148, #42149, #23934, #29031, #71996, #91335, #145749, #199082, #124499 ) ) ;
#110052=CARTESIAN_POINT ( 'NONE',  ( -16.97092634996705485, 10.00088896636034264, -79.63014276629733956 ) ) ;
#110065=DIRECTION ( 'NONE',  ( 1.000000000000000000, -0.000000000000000000, -0.000000000000000000 ) ) ;
#110142=ADVANCED_FACE ( 'NONE', ( #101589 ), #135609, .T. ) ;
#110144=PLANE ( 'NONE',  #201550 ) ;
#110453=PLANE ( 'NONE',  #210817 ) ;
#110535=DIRECTION ( 'NONE',  ( 1.073024830501117725E-15, 0.000000000000000000, 1.000000000000000000 ) ) ;
#110758=ORIENTED_EDGE ( 'NONE', *, *, #111779, .F. ) ;
#110837=ORIENTED_EDGE ( 'NONE', *, *, #96995, .F. ) ;
#111034=ORIENTED_EDGE ( 'NONE', *, *, #153315, .T. ) ;
#111153=CARTESIAN_POINT ( 'NONE',  ( -23.25000000000000355, 11.75000000001113953, -76.25000000000004263 ) ) ;
#111246=AXIS2_PLACEMENT_3D ( 'NONE', #116345, #134583, #158076 ) ;
#111321=CARTESIAN_POINT ( 'NONE',  ( -16.92507428761699018, 9.950000000011140600, -87.78660254037849597 ) ) ;
#111367=CARTESIAN_POINT ( 'NONE',  ( -16.94309007106719989, 9.992226192581140864, -79.60579128255554338 ) ) ;
#111644=CARTESIAN_POINT ( 'NONE',  ( -14.22969084473440304, 9.456007326080463571, -85.48863349414676804 ) ) ;
#111697=ORIENTED_EDGE ( 'NONE', *, *, #205331, .T. ) ;
#111779=EDGE_CURVE ( 'NONE', #198491, #13912, #60480, .T. ) ;
#111805=EDGE_CURVE ( 'NONE', #72719, #54282, #56604, .T. ) ;
#111959=ORIENTED_EDGE ( 'NONE', *, *, #82807, .T. ) ;
#112108=CARTESIAN_POINT ( 'NONE',  ( -23.25000000000000355, 11.75000000001113953, -87.85000000000003695 ) ) ;
#112207=CARTESIAN_POINT ( 'NONE',  ( 15.73863059295127798, 9.351403174152808973, -83.97953043683850183 ) ) ;
#112486=CARTESIAN_POINT ( 'NONE',  ( 15.48841904831874849, 8.561580951692381092, -87.85000000000005116 ) ) ;
#112694=ORIENTED_EDGE ( 'NONE', *, *, #191024, .T. ) ;
#112749=VERTEX_POINT ( 'NONE', #205820 ) ;
#112776=CIRCLE ( 'NONE', #191913, 0.1000000000000001305 ) ;
#112804=CARTESIAN_POINT ( 'NONE',  ( -14.87779219673429054, 9.430633469083952392, -82.23176579482412762 ) ) ;
#112903=EDGE_LOOP ( 'NONE', ( #52422, #26913, #193236, #196313 ) ) ;
#112905=CYLINDRICAL_SURFACE ( 'NONE', #180646, 0.09999999999999939493 ) ;
#112964=LINE ( 'NONE', #135065, #109564 ) ;
#113111=CARTESIAN_POINT ( 'NONE',  ( -18.40000000000000213, 5.650000000011139001, -91.25000000000005684 ) ) ;
#113535=EDGE_CURVE ( 'NONE', #201212, #146715, #159059, .T. ) ;
#113632=ORIENTED_EDGE ( 'NONE', *, *, #167466, .F. ) ;
#113715=ORIENTED_EDGE ( 'NONE', *, *, #180393, .F. ) ;
#113927=CARTESIAN_POINT ( 'NONE',  ( -16.93440969289731513, 9.995185175825110235, -79.59123418501083336 ) ) ;
#114016=ORIENTED_EDGE ( 'NONE', *, *, #215165, .F. ) ;
#114131=EDGE_LOOP ( 'NONE', ( #7244, #125461, #13389, #101463 ) ) ;
#114157=CARTESIAN_POINT ( 'NONE',  ( -16.87683809663752399, 9.864913447291341342, -87.22428155130397442 ) ) ;
#114187=VECTOR ( 'NONE', #247299, 1000.000000000000000 ) ;
#114209=AXIS2_PLACEMENT_3D ( 'NONE', #162600, #221258, #240850 ) ;
#114220=CARTESIAN_POINT ( 'NONE',  ( 20.05000000000002913, 7.250000000011171508, -87.85000000000003695 ) ) ;
#114278=( GEOMETRIC_REPRESENTATION_CONTEXT ( 3 ) GLOBAL_UNCERTAINTY_ASSIGNED_CONTEXT ( ( #227720 ) ) GLOBAL_UNIT_ASSIGNED_CONTEXT ( ( #7090, #86608, #178385 ) ) REPRESENTATION_CONTEXT ( 'NONE', 'WORKASPACE' ) );
#114306=FACE_OUTER_BOUND ( 'NONE', #72655, .T. ) ;
#114583=CYLINDRICAL_SURFACE ( 'NONE', #219656, 1.500000000000001332 ) ;
#114754=CARTESIAN_POINT ( 'NONE',  ( 15.51872946208854920, 9.376580978055097049, -84.62694624701198620 ) ) ;
#114889=( BOUNDED_CURVE ( )  B_SPLINE_CURVE ( 3, ( #151754, #30515, #111321, #188277 ),
 .UNSPECIFIED., .F., .F. ) 
 B_SPLINE_CURVE_WITH_KNOTS ( ( 4, 4 ),
 ( 1.570796326794908992, 2.617993877991549034 ),
 .UNSPECIFIED. ) 
 CURVE ( )  GEOMETRIC_REPRESENTATION_ITEM ( )  RATIONAL_B_SPLINE_CURVE ( ( 1.000000000000000000, 0.9106836025229521070, 0.9106836025229521070, 1.000000000000000000 ) ) 
 REPRESENTATION_ITEM ( '' )  );
#115164=CARTESIAN_POINT ( 'NONE',  ( -16.77308656112214535, 9.950000000011135270, -79.65019319170235690 ) ) ;
#115205=ORIENTED_EDGE ( 'NONE', *, *, #91326, .T. ) ;
#115418=CARTESIAN_POINT ( 'NONE',  ( -20.65000000000000568, 7.250000000011138646, -87.85000000000003695 ) ) ;
#115514=CARTESIAN_POINT ( 'NONE',  ( -16.94445028196808778, 9.992063609708889516, -79.60733017841850767 ) ) ;
#115600=VECTOR ( 'NONE', #104639, 1000.000000000000000 ) ;
#115840=ORIENTED_EDGE ( 'NONE', *, *, #177789, .T. ) ;
#115879=ORIENTED_EDGE ( 'NONE', *, *, #162245, .F. ) ;
#116052=CARTESIAN_POINT ( 'NONE',  ( 12.25000000000000000, 9.350000000011140955, -83.75000000000004263 ) ) ;
#116137=CARTESIAN_POINT ( 'NONE',  ( -18.36973785203556275, 11.47550320049537476, -91.25000000000005684 ) ) ;
#116345=CARTESIAN_POINT ( 'NONE',  ( 21.72449340488910252, 10.28395627750227526, -76.25000000000004263 ) ) ;
#116393=ORIENTED_EDGE ( 'NONE', *, *, #102963, .F. ) ;
#116460=( BOUNDED_SURFACE ( )  B_SPLINE_SURFACE ( 3, 2, ( 
 ( #201374, #3156, #85247 ),
 ( #125690, #44879, #124424 ),
 ( #240504, #164833, #61877 ),
 ( #46153, #43597, #7030 ),
 ( #65720, #146521, #224778 ),
 ( #141398, #205214, #220922 ),
 ( #183115, #42308, #203946 ),
 ( #206519, #222198, #121856 ),
 ( #4451, #244347, #145245 ),
 ( #83948, #47425, #26620 ) ),
 .UNSPECIFIED., .F., .F., .F. ) 
 B_SPLINE_SURFACE_WITH_KNOTS ( ( 4, 2, 2, 2, 4 ),
 ( 3, 3 ),
 ( 0.002161241639767248670, 0.002579950749615824400, 0.002789305304540112482, 0.002893982582002256523, 0.002998659859464400564 ),
 ( 0.000000000000000000, 1.000000000000000000 ),
 .UNSPECIFIED. ) 
 GEOMETRIC_REPRESENTATION_ITEM ( )  RATIONAL_B_SPLINE_SURFACE ( (
 ( 1.000000000000000000, 0.7071067811865536790, 1.000000000000000000),
 ( 1.000000000000000000, 0.7632447400666954040, 1.000000000000000000),
 ( 1.000000000000000000, 0.8158073005106659670, 1.000000000000000000),
 ( 1.000000000000000000, 0.8906973462397590469, 1.000000000000000000),
 ( 1.000000000000000000, 0.9149408947800071745, 1.000000000000000000),
 ( 1.000000000000000000, 0.9493368785275861921, 1.000000000000000000),
 ( 1.000000000000000000, 0.9605194247156703113, 1.000000000000000000),
 ( 1.000000000000000000, 0.9803630264781235670, 1.000000000000000000),
 ( 1.000000000000000000, 0.9900844824271131106, 1.000000000000000000),
 ( 1.000000000000000000, 0.9894588281429246290, 1.000000000000000000) ) ) 
 REPRESENTATION_ITEM ( '' )  SURFACE ( )  );
#116628=B_SPLINE_CURVE_WITH_KNOTS ( 'NONE', 3,
 ( #220211, #121135, #149345, #208029, #210580, #72371, #188440, #247120, #211880, #50201 ),
 .UNSPECIFIED., .F., .F.,
 ( 4, 2, 2, 2, 4 ),
 ( 5.273673492279070357E-16, 9.930191194501526101E-05, 0.0001986038238895031390, 0.0003972076477784386439, 0.0007944152955563512329 ),
 .UNSPECIFIED. ) ;
#116814=CARTESIAN_POINT ( 'NONE',  ( -16.91256925476569606, 9.985731158139328656, -87.96764248900531413 ) ) ;
#116852=CARTESIAN_POINT ( 'NONE',  ( -16.27683809663751191, 9.350000000011133849, -76.25000000000001421 ) ) ;
#117728=FACE_OUTER_BOUND ( 'NONE', #40269, .T. ) ;
#117754=CARTESIAN_POINT ( 'NONE',  ( -16.78493832629887450, 9.945835743215301505, -79.66394901910423698 ) ) ;
#117763=EDGE_CURVE ( 'NONE', #54282, #171691, #197722, .T. ) ;
#117785=VECTOR ( 'NONE', #86493, 1000.000000000000000 ) ;
#117827=CARTESIAN_POINT ( 'NONE',  ( -16.97683809663752186, 9.950000000011138823, -80.40236401819653622 ) ) ;
#118184=SURFACE_STYLE_FILL_AREA ( #236835 ) ;
#118442=CARTESIAN_POINT ( 'NONE',  ( 20.04999999999999716, 8.750000000011173285, -76.25000000000004263 ) ) ;
#118566=ORIENTED_EDGE ( 'NONE', *, *, #170187, .F. ) ;
#118632=DIRECTION ( 'NONE',  ( 1.186688945009010077E-16, -1.000000000000000000, -0.000000000000000000 ) ) ;
#118810=EDGE_LOOP ( 'NONE', ( #193866, #198649, #48053, #208399 ) ) ;
#119033=CARTESIAN_POINT ( 'NONE',  ( 15.74999999999999645, 9.850000000011137402, -83.75000000000004263 ) ) ;
#119055=CARTESIAN_POINT ( 'NONE',  ( 23.24999999999999645, 11.75000000001113953, -76.25000000000004263 ) ) ;
#119121=ORIENTED_EDGE ( 'NONE', *, *, #87893, .T. ) ;
#119254=CARTESIAN_POINT ( 'NONE',  ( -18.40000000000000213, 11.75000000001113953, -79.65000000000004832 ) ) ;
#119323=CARTESIAN_POINT ( 'NONE',  ( -16.77977881697927032, 9.946601933544062746, -79.66137857311510118 ) ) ;
#119688=ORIENTED_EDGE ( 'NONE', *, *, #204859, .T. ) ;
#119768=ORIENTED_EDGE ( 'NONE', *, *, #138212, .T. ) ;
#119851=( BOUNDED_CURVE ( )  B_SPLINE_CURVE ( 3, ( #24916, #180127, #1466, #21073 ),
 .UNSPECIFIED., .F., .T. ) 
 B_SPLINE_CURVE_WITH_KNOTS ( ( 4, 4 ),
 ( 4.712388980384689674, 5.672655318024644622 ),
 .UNSPECIFIED. ) 
 CURVE ( )  GEOMETRIC_REPRESENTATION_ITEM ( )  RATIONAL_B_SPLINE_CURVE ( ( 1.000000000000000000, 0.9246222802177426203, 0.9246222802177426203, 1.000000000000000000 ) ) 
 REPRESENTATION_ITEM ( '' )  );
#119875=CARTESIAN_POINT ( 'NONE',  ( 14.45204356427542081, 9.450668889178686527, -82.05554649020737656 ) ) ;
#119947=DIRECTION ( 'NONE',  ( -1.000000000000000000, 0.000000000000000000, 0.000000000000000000 ) ) ;
#119987=ORIENTED_EDGE ( 'NONE', *, *, #47963, .F. ) ;
#120031=LINE ( 'NONE', #177439, #23139 ) ;
#120089=EDGE_CURVE ( 'NONE', #146041, #207925, #199749, .T. ) ;
#120126=CARTESIAN_POINT ( 'NONE',  ( 17.74533788810830615, 10.81849979148195118, -77.31362267494763785 ) ) ;
#120366=CARTESIAN_POINT ( 'NONE',  ( -16.79139129368504157, 9.944944162472836524, -79.67024463282588442 ) ) ;
#120501=LINE ( 'NONE', #257345, #132968 ) ;
#120586=LINE ( 'NONE', #115418, #189077 ) ;
#120644=CARTESIAN_POINT ( 'NONE',  ( -16.87786941232800686, 9.958154714156124854, -87.87718579979406286 ) ) ;
#121135=CARTESIAN_POINT ( 'NONE',  ( -16.84419801905645997, 9.950000000011140600, -87.83051015377803594 ) ) ;
#121163=CARTESIAN_POINT ( 'NONE',  ( 13.99999999999999822, 9.850000000011137402, -83.75000000000004263 ) ) ;
#121170=CARTESIAN_POINT ( 'NONE',  ( 15.75000000000000000, 9.350000000011139178, -83.51856895740272080 ) ) ;
#121254=EDGE_CURVE ( 'NONE', #3745, #203569, #167777, .T. ) ;
#121362=ORIENTED_EDGE ( 'NONE', *, *, #206794, .T. ) ;
#121637=CARTESIAN_POINT ( 'NONE',  ( -16.83794237512074687, 9.926359221118632448, -79.80354215869901680 ) ) ;
#121772=CARTESIAN_POINT ( 'NONE',  ( -18.39999999999999858, 11.47316190337362762, -76.32594606680801519 ) ) ;
#121802=LINE ( 'NONE', #83895, #132656 ) ;
#121848=DIRECTION ( 'NONE',  ( -1.000000000000000000, 0.000000000000000000, 0.000000000000000000 ) ) ;
#121856=CARTESIAN_POINT ( 'NONE',  ( -16.83558968593875349, 9.950000000011137047, -87.83769481238333299 ) ) ;
#121902=CARTESIAN_POINT ( 'NONE',  ( -16.77828822508139694, 9.946229374931901290, -79.66262825137400228 ) ) ;
#122143=CARTESIAN_POINT ( 'NONE',  ( -16.92570016628983254, 9.958788957751014692, -87.87934932996105886 ) ) ;
#122219=CARTESIAN_POINT ( 'NONE',  ( -18.40000000000000213, 5.650000000011139001, -87.85000000000003695 ) ) ;
#122424=CARTESIAN_POINT ( 'NONE',  ( 14.87567385445976953, 9.430764995433476017, -82.23053739475051316 ) ) ;
#122580=( BOUNDED_CURVE ( )  B_SPLINE_CURVE ( 3, ( #247612, #127674, #28622, #128958 ),
 .UNSPECIFIED., .F., .F. ) 
 B_SPLINE_CURVE_WITH_KNOTS ( ( 4, 4 ),
 ( 0.5235987755983128045, 1.570796326794896558 ),
 .UNSPECIFIED. ) 
 CURVE ( )  GEOMETRIC_REPRESENTATION_ITEM ( )  RATIONAL_B_SPLINE_CURVE ( ( 1.000000000000000000, 0.9106836025229614329, 0.9106836025229614329, 1.000000000000000000 ) ) 
 REPRESENTATION_ITEM ( '' )  );
#122848=CARTESIAN_POINT ( 'NONE',  ( -16.80469485234341676, 9.942151663152195340, -87.80996684393123530 ) ) ;
#122865=CARTESIAN_POINT ( 'NONE',  ( -18.40000000000000213, 8.822561741677553471, -76.25000000000004263 ) ) ;
#123080=DIRECTION ( 'NONE',  ( 1.020425574104004196E-15, 1.210927747993693964E-31, -1.000000000000000000 ) ) ;
#123225=VECTOR ( 'NONE', #199113, 1000.000000000000000 ) ;
#123257=ORIENTED_EDGE ( 'NONE', *, *, #102963, .T. ) ;
#123405=DIRECTION ( 'NONE',  ( -1.000000000000000000, 0.000000000000000000, 0.000000000000000000 ) ) ;
#123504=CARTESIAN_POINT ( 'NONE',  ( -17.11825945287481332, 10.05000000001113847, -87.85000000000003695 ) ) ;
#123608=CARTESIAN_POINT ( 'NONE',  ( -16.87036670365549895, 9.989418819312803066, -79.52043988269799968 ) ) ;
#123671=DIRECTION ( 'NONE',  ( 1.000000000000000000, 0.000000000000000000, 0.000000000000000000 ) ) ;
#123684=ORIENTED_EDGE ( 'NONE', *, *, #136889, .F. ) ;
#123763=PRODUCT_CONTEXT ( 'NONE', #180708, 'mechanical' ) ;
#123773=DIRECTION ( 'NONE',  ( 0.000000000000000000, 1.000000000000000000, -0.000000000000000000 ) ) ;
#123895=CARTESIAN_POINT ( 'NONE',  ( -16.89268316805466341, 9.951721813253341153, -79.64424752145448849 ) ) ;
#124016=CARTESIAN_POINT ( 'NONE',  ( -16.94052228080551359, 9.986279733109993728, -87.89037550266947108 ) ) ;
#124034=CARTESIAN_POINT ( 'NONE',  ( 18.39999999999999503, 11.75000000001113953, -79.65000000000004832 ) ) ;
#124326=FACE_OUTER_BOUND ( 'NONE', #216144, .T. ) ;
#124424=CARTESIAN_POINT ( 'NONE',  ( -16.97683810757273193, 9.950000000011137047, -87.23642328753973629 ) ) ;
#124497=ORIENTED_EDGE ( 'NONE', *, *, #161626, .F. ) ;
#124499=ORIENTED_EDGE ( 'NONE', *, *, #6574, .F. ) ;
#124769=ORIENTED_EDGE ( 'NONE', *, *, #157840, .F. ) ;
#124811=CARTESIAN_POINT ( 'NONE',  ( -18.40000000000000213, 11.47316190337364183, -87.95000000000004547 ) ) ;
#125057=DIRECTION ( 'NONE',  ( 0.000000000000000000, 0.000000000000000000, 1.000000000000000000 ) ) ;
#125073=DIRECTION ( 'NONE',  ( 1.000000000000000000, 1.186688945009010077E-16, 0.000000000000000000 ) ) ;
#125222=ORIENTED_EDGE ( 'NONE', *, *, #212464, .T. ) ;
#125346=LINE ( 'NONE', #119254, #176224 ) ;
#125461=ORIENTED_EDGE ( 'NONE', *, *, #257021, .T. ) ;
#125690=CARTESIAN_POINT ( 'NONE',  ( -16.87683809663752399, 9.865889849343686180, -87.23257319293058742 ) ) ;
#125722=DIRECTION ( 'NONE',  ( 0.000000000000000000, 0.000000000000000000, -1.000000000000000000 ) ) ;
#125903=VERTEX_POINT ( 'NONE', #152025 ) ;
#126000=FACE_OUTER_BOUND ( 'NONE', #153502, .T. ) ;
#126357=EDGE_CURVE ( 'NONE', #66750, #185693, #161993, .T. ) ;
#126591=CARTESIAN_POINT ( 'NONE',  ( -16.93860193097148326, 9.993107767340399405, -87.90013836730690855 ) ) ;
#126692=CARTESIAN_POINT ( 'NONE',  ( 18.54999999999999716, 8.750000000011182166, -87.85000000000003695 ) ) ;
#127073=ORIENTED_EDGE ( 'NONE', *, *, #246257, .F. ) ;
#127239=ORIENTED_EDGE ( 'NONE', *, *, #127354, .T. ) ;
#127354=EDGE_CURVE ( 'NONE', #219674, #218042, #237234, .T. ) ;
#127519=ORIENTED_EDGE ( 'NONE', *, *, #200142, .F. ) ;
#127581=ORIENTED_EDGE ( 'NONE', *, *, #43022, .T. ) ;
#127622=PLANE ( 'NONE',  #9001 ) ;
#127674=CARTESIAN_POINT ( 'NONE',  ( -16.92507428761701505, 9.950000000011138823, -79.71339745962158929 ) ) ;
#127745=CARTESIAN_POINT ( 'NONE',  ( -16.88219499860498374, 9.950206425438743452, -79.64930969010735851 ) ) ;
#127881=CARTESIAN_POINT ( 'NONE',  ( -16.93262454970419384, 10.00202046794151478, -87.92707622623736086 ) ) ;
#127967=AXIS2_PLACEMENT_3D ( 'NONE', #10101, #53067, #192590 ) ;
#128019=CARTESIAN_POINT ( 'NONE',  ( -23.25000000000000355, 11.75000000001113953, -76.25000000000004263 ) ) ;
#128159=VERTEX_POINT ( 'NONE', #58407 ) ;
#128187=CARTESIAN_POINT ( 'NONE',  ( -16.81744102076748959, 9.950000000011138823, -87.85000000000005116 ) ) ;
#128363=B_SPLINE_CURVE_WITH_KNOTS ( 'NONE', 3,
 ( #242657, #202263, #180141, #26203, #143562, #124016, #103136, #105690, #163147, #183976, #165720, #182713, #81003 ),
 .UNSPECIFIED., .F., .F.,
 ( 4, 3, 3, 3, 4 ),
 ( -3.224855718275878119E-06, 0.000000000000000000, 6.199515528665969596E-06, 4.034952380127002048E-05, 7.452715123699844260E-05 ),
 .UNSPECIFIED. ) ;
#128455=ORIENTED_EDGE ( 'NONE', *, *, #214480, .F. ) ;
#128516=CARTESIAN_POINT ( 'NONE',  ( -15.52965525596987995, 9.375538102059159939, -82.86987588099090374 ) ) ;
#128841=ORIENTED_EDGE ( 'NONE', *, *, #211534, .T. ) ;
#128958=CARTESIAN_POINT ( 'NONE',  ( -17.11825945287482753, 9.950000000011138823, -79.75000000000004263 ) ) ;
#128977=DIRECTION ( 'NONE',  ( -1.000000000000000000, 0.000000000000000000, 0.000000000000000000 ) ) ;
#129098=ADVANCED_FACE ( 'NONE', ( #238415 ), #257923, .F. ) ;
#129234=EDGE_CURVE ( 'NONE', #108130, #68524, #206287, .T. ) ;
#129237=CARTESIAN_POINT ( 'NONE',  ( -18.40000000000000213, 11.75000000001113953, -79.65000000000004832 ) ) ;
#129272=VERTEX_POINT ( 'NONE', #25786 ) ;
#129347=VECTOR ( 'NONE', #26994, 1000.000000000000000 ) ;
#129876=CARTESIAN_POINT ( 'NONE',  ( -16.78055652883087134, 9.946776916136505164, -79.66079183759246973 ) ) ;
#129912=CARTESIAN_POINT ( 'NONE',  ( -14.87770893841226894, 9.430637101707898040, -85.26826061806100654 ) ) ;
#130023=CYLINDRICAL_SURFACE ( 'NONE', #127967, 1.749999999999999778 ) ;
#130370=EDGE_LOOP ( 'NONE', ( #183598, #146359, #257356, #249498 ) ) ;
#130466=VERTEX_POINT ( 'NONE', #83528 ) ;
#130597=AXIS2_PLACEMENT_3D ( 'NONE', #33855, #134177, #55904 ) ;
#130754=ORIENTED_EDGE ( 'NONE', *, *, #203629, .T. ) ;
#130817=APPLICATION_CONTEXT ( 'automotive_design' ) ;
#130899=VECTOR ( 'NONE', #17244, 999.9999999999998863 ) ;
#130908=EDGE_CURVE ( 'NONE', #8126, #185121, #116628, .T. ) ;
#130928=CARTESIAN_POINT ( 'NONE',  ( -16.93226657140833069, 9.999543822735571297, -79.57871311097366629 ) ) ;
#130963=ORIENTED_EDGE ( 'NONE', *, *, #246257, .T. ) ;
#131024=MECHANICAL_DESIGN_GEOMETRIC_PRESENTATION_REPRESENTATION('',(#255886),#114278);
#131112=EDGE_CURVE ( 'NONE', #97884, #39296, #77454, .T. ) ;
#131569=B_SPLINE_CURVE_WITH_KNOTS ( 'NONE', 3,
 ( #54136, #94545, #150685, #30762 ),
 .UNSPECIFIED., .F., .F.,
 ( 4, 4 ),
 ( 0.000000000000000000, 7.713889350929433657E-05 ),
 .UNSPECIFIED. ) ;
#131742=CARTESIAN_POINT ( 'NONE',  ( 13.43663047529820709, 9.446645344706402270, -85.41080645610021804 ) ) ;
#131903=PRODUCT_DEFINITION_CONTEXT ( 'detailed design', #130817, 'design' ) ;
#132074=ADVANCED_BREP_SHAPE_REPRESENTATION ( '', ( #197609, #2425 ), #27429 ) ;
#132336=AXIS2_PLACEMENT_3D ( 'NONE', #158387, #177929, #59203 ) ;
#132360=CARTESIAN_POINT ( 'NONE',  ( -15.39946565075090668, 9.389534562357859215, -82.67480930438999565 ) ) ;
#132656=VECTOR ( 'NONE', #123080, 1000.000000000000000 ) ;
#132968=VECTOR ( 'NONE', #198717, 1000.000000000000000 ) ;
#133024=CARTESIAN_POINT ( 'NONE',  ( 18.39999999999998082, 11.47316190337362585, -76.25000000000004263 ) ) ;
#133430=DIRECTION ( 'NONE',  ( 1.000000000000000000, 0.000000000000000000, 0.000000000000000000 ) ) ;
#133495=CARTESIAN_POINT ( 'NONE',  ( -16.93262454970420094, 10.00202046794151300, -79.57292377376273862 ) ) ;
#133928=FACE_OUTER_BOUND ( 'NONE', #90163, .T. ) ;
#134177=DIRECTION ( 'NONE',  ( -1.073024830501117725E-15, 0.000000000000000000, 1.000000000000000000 ) ) ;
#134308=VECTOR ( 'NONE', #123405, 1000.000000000000000 ) ;
#134349=EDGE_LOOP ( 'NONE', ( #202839, #244159, #244240, #53971, #155123, #211504, #222612, #184393, #118566 ) ) ;
#134381=LINE ( 'NONE', #17043, #162602 ) ;
#134549=VERTEX_POINT ( 'NONE', #140555 ) ;
#134583=DIRECTION ( 'NONE',  ( 0.8049926720990051576, 0.5932847527679298016, -0.000000000000000000 ) ) ;
#134584=VERTEX_POINT ( 'NONE', #238379 ) ;
#134997=CARTESIAN_POINT ( 'NONE',  ( -16.79184697841823493, 9.948761661669548673, -79.65414227060256280 ) ) ;
#135065=CARTESIAN_POINT ( 'NONE',  ( 15.48841904831874849, 8.561580951692381092, -79.65000000000003411 ) ) ;
#135160=DIRECTION ( 'NONE',  ( 0.000000000000000000, 0.000000000000000000, 1.000000000000000000 ) ) ;
#135346=ADVANCED_FACE ( 'NONE', ( #100782 ), #65546, .F. ) ;
#135578=CARTESIAN_POINT ( 'NONE',  ( 15.39170923737819585, 9.389529397477893724, -84.81710791289373219 ) ) ;
#135609=CYLINDRICAL_SURFACE ( 'NONE', #28743, 0.1000000000000028644 ) ;
#135640=EDGE_CURVE ( 'NONE', #31733, #175274, #217557, .T. ) ;
#135794=CYLINDRICAL_SURFACE ( 'NONE', #152879, 0.1000000000000028644 ) ;
#135804=DIRECTION ( 'NONE',  ( -1.000000000000000000, 0.000000000000000000, 0.000000000000000000 ) ) ;
#135945=AXIS2_PLACEMENT_3D ( 'NONE', #54264, #215895, #178098 ) ;
#136284=DIRECTION ( 'NONE',  ( -1.000000000000000000, 0.000000000000000000, 0.000000000000000000 ) ) ;
#136431=SURFACE_SIDE_STYLE ('',( #118184 ) ) ;
#136460=CARTESIAN_POINT ( 'NONE',  ( -16.92209698673556062, 9.950000000011138823, -87.78936443294738012 ) ) ;
#136818=VECTOR ( 'NONE', #224756, 1000.000000000000000 ) ;
#136834=CARTESIAN_POINT ( 'NONE',  ( 12.29592348164039350, 9.355806591641286474, -83.29110253154621546 ) ) ;
#136887=ORIENTED_EDGE ( 'NONE', *, *, #79507, .F. ) ;
#136889=EDGE_CURVE ( 'NONE', #128159, #38688, #180285, .T. ) ;
#136898=CARTESIAN_POINT ( 'NONE',  ( -20.65000000000000568, 5.650000000011139001, -76.25000000000004263 ) ) ;
#136949=DIRECTION ( 'NONE',  ( -0.000000000000000000, -0.000000000000000000, -1.000000000000000000 ) ) ;
#137050=( BOUNDED_CURVE ( )  B_SPLINE_CURVE ( 3, ( #242439, #178666, #63823, #143347 ),
 .UNSPECIFIED., .F., .T. ) 
 B_SPLINE_CURVE_WITH_KNOTS ( ( 4, 4 ),
 ( 5.733388419619901200, 5.983100554402348337 ),
 .UNSPECIFIED. ) 
 CURVE ( )  GEOMETRIC_REPRESENTATION_ITEM ( )  RATIONAL_B_SPLINE_CURVE ( ( 1.000000000000000000, 0.9948104011409416580, 0.9948104011409416580, 1.000000000000000000 ) ) 
 REPRESENTATION_ITEM ( '' )  );
#137058=LINE ( 'NONE', #195776, #139462 ) ;
#137096=DIRECTION ( 'NONE',  ( 0.000000000000000000, 0.000000000000000000, -1.000000000000000000 ) ) ;
#137135=VECTOR ( 'NONE', #1483, 1000.000000000000000 ) ;
#137281=CARTESIAN_POINT ( 'NONE',  ( -16.96982749440708460, 9.950000000011137047, -80.12477840881192037 ) ) ;
#137294=EDGE_CURVE ( 'NONE', #65351, #201212, #120031, .T. ) ;
#137589=CARTESIAN_POINT ( 'NONE',  ( -16.86379686415369150, 9.975217759264314310, -87.93338988909033560 ) ) ;
#137908=EDGE_CURVE ( 'NONE', #222707, #125903, #154002, .T. ) ;
#137920=ORIENTED_EDGE ( 'NONE', *, *, #214480, .T. ) ;
#137946=EDGE_CURVE ( 'NONE', #59523, #28760, #112964, .T. ) ;
#138107=CARTESIAN_POINT ( 'NONE',  ( 12.47034474403012183, 9.375538102059158163, -82.86987588099087532 ) ) ;
#138212=EDGE_CURVE ( 'NONE', #39296, #81779, #184469, .T. ) ;
#138298=EDGE_CURVE ( 'NONE', #125903, #32954, #35734, .T. ) ;
#138558=DIRECTION ( 'NONE',  ( -1.000000000000000000, 0.000000000000000000, 0.000000000000000000 ) ) ;
#138838=CARTESIAN_POINT ( 'NONE',  ( -16.77779411503079032, 9.946101446935278645, -79.66305741761988202 ) ) ;
#138868=CARTESIAN_POINT ( 'NONE',  ( 16.87683809663750267, 9.950000000011138823, -79.65000000000003411 ) ) ;
#138941=DIRECTION ( 'NONE',  ( -1.020425574104004196E-15, -1.210927747993693964E-31, -1.000000000000000000 ) ) ;
#139028=CARTESIAN_POINT ( 'NONE',  ( -18.40000000000000213, 11.47316190337362762, -79.65000000000004832 ) ) ;
#139306=DIRECTION ( 'NONE',  ( 1.000000000000000000, 0.000000000000000000, 0.000000000000000000 ) ) ;
#139335=ORIENTED_EDGE ( 'NONE', *, *, #49242, .T. ) ;
#139388=CARTESIAN_POINT ( 'NONE',  ( 13.12220780326571123, 9.430633469083950615, -82.23176579482412762 ) ) ;
#139462=VECTOR ( 'NONE', #214034, 1000.000000000000000 ) ;
#139685=VECTOR ( 'NONE', #32320, 1000.000000000000000 ) ;
#139964=PLANE ( 'NONE',  #157380 ) ;
#140067=DIRECTION ( 'NONE',  ( -1.000000000000000000, 0.000000000000000000, 0.000000000000000000 ) ) ;
#140282=EDGE_LOOP ( 'NONE', ( #87806, #124769, #161390, #229338, #161771 ) ) ;
#140397=CARTESIAN_POINT ( 'NONE',  ( -17.11825945287481332, 10.05000000001113847, -87.75000000000005684 ) ) ;
#140555=CARTESIAN_POINT ( 'NONE',  ( -21.64999999999999858, 10.05000000001113847, -87.85000000000003695 ) ) ;
#140586=CARTESIAN_POINT ( 'NONE',  ( -17.71734398241073905, 10.84235722847571814, -77.27486174699446053 ) ) ;
#140767=CARTESIAN_POINT ( 'NONE',  ( -18.40000000000000213, 11.47316190337362762, -79.55000000000005400 ) ) ;
#140917=ORIENTED_EDGE ( 'NONE', *, *, #235090, .F. ) ;
#141169=ORIENTED_EDGE ( 'NONE', *, *, #129234, .T. ) ;
#141250=CARTESIAN_POINT ( 'NONE',  ( -16.89020380669786547, 9.950000000011137047, -79.75741114811062005 ) ) ;
#141398=CARTESIAN_POINT ( 'NONE',  ( -16.83233564386403458, 9.930221796595763095, -87.72452066347565847 ) ) ;
#141492=VECTOR ( 'NONE', #50757, 1000.000000000000000 ) ;
#141687=CARTESIAN_POINT ( 'NONE',  ( -16.94878442675511465, 9.991729103002157331, -87.88821957563791898 ) ) ;
#141787=CARTESIAN_POINT ( 'NONE',  ( -18.40000000000000213, 11.47316190337364183, -87.89142135623735896 ) ) ;
#141870=DIRECTION ( 'NONE',  ( 0.000000000000000000, 0.000000000000000000, -1.000000000000000000 ) ) ;
#141917=EDGE_CURVE ( 'NONE', #31733, #146041, #230390, .T. ) ;
#141993=ORIENTED_EDGE ( 'NONE', *, *, #51435, .T. ) ;
#142109=AXIS2_PLACEMENT_3D ( 'NONE', #199171, #197877, #38826 ) ;
#142376=DIRECTION ( 'NONE',  ( -0.000000000000000000, -0.000000000000000000, -1.000000000000000000 ) ) ;
#142406=DIRECTION ( 'NONE',  ( 0.000000000000000000, 0.000000000000000000, 1.000000000000000000 ) ) ;
#142514=CARTESIAN_POINT ( 'NONE',  ( -16.92989143108098204, 9.950000000011138823, -79.88248387475671564 ) ) ;
#142531=EDGE_CURVE ( 'NONE', #3167, #28760, #108234, .T. ) ;
#142584=CARTESIAN_POINT ( 'NONE',  ( -16.77828822459933633, 9.946229375067616729, -87.83737174908110035 ) ) ;
#142597=EDGE_CURVE ( 'NONE', #175274, #54282, #161101, .T. ) ;
#143075=( BOUNDED_SURFACE ( )  B_SPLINE_SURFACE ( 3, 2, ( 
 ( #94325, #173926, #74816 ),
 ( #89191, #248277, #69656 ),
 ( #19954, #99446, #21254 ),
 ( #100715, #362, #76052 ) ),
 .UNSPECIFIED., .F., .F., .F. ) 
 B_SPLINE_SURFACE_WITH_KNOTS ( ( 4, 4 ),
 ( 3, 3 ),
 ( 0.0008258556059633901563, 0.0009616864997632837159 ),
 ( 0.000000000000000000, 1.000000000000000000 ),
 .UNSPECIFIED. ) 
 GEOMETRIC_REPRESENTATION_ITEM ( )  RATIONAL_B_SPLINE_SURFACE ( (
 ( 1.000000000000000000, 0.9152888060719349683, 1.000000000000000000),
 ( 1.000000000000000000, 0.9327727094138192898, 1.000000000000000000),
 ( 1.000000000000000000, 0.9369023509258407323, 1.000000000000000000),
 ( 1.000000000000000000, 0.9246339933864529126, 1.000000000000000000) ) ) 
 REPRESENTATION_ITEM ( '' )  SURFACE ( )  );
#143079=ADVANCED_FACE ( 'NONE', ( #92192 ), #130023, .F. ) ;
#143299=DIRECTION ( 'NONE',  ( 1.000000000000000000, 0.000000000000000000, 0.000000000000000000 ) ) ;
#143347=CARTESIAN_POINT ( 'NONE',  ( -16.94107738177414291, 10.01423928514777373, -87.95000000000004547 ) ) ;
#143362=VERTEX_POINT ( 'NONE', #241976 ) ;
#143441=CARTESIAN_POINT ( 'NONE',  ( -16.87331047859651179, 9.950000000011142376, -79.65000000000004832 ) ) ;
#143562=CARTESIAN_POINT ( 'NONE',  ( -16.94165728009537375, 9.987869755934930538, -87.89105500851024999 ) ) ;
#143572=LINE ( 'NONE', #160601, #137135 ) ;
#143796=CARTESIAN_POINT ( 'NONE',  ( 20.99999999999999645, 9.750000000011137757, -76.25000000000004263 ) ) ;
#143848=VERTEX_POINT ( 'NONE', #240996 ) ;
#143866=CARTESIAN_POINT ( 'NONE',  ( -17.29158576265544056, 10.36474766602906783, -78.41724175520788265 ) ) ;
#144442=VECTOR ( 'NONE', #14645, 1000.000000000000000 ) ;
#144639=ADVANCED_FACE ( 'NONE', ( #198677 ), #139964, .F. ) ;
#144660=LINE ( 'NONE', #65128, #21829 ) ;
#144701=DIRECTION ( 'NONE',  ( 1.000000000000000000, 0.000000000000000000, 0.000000000000000000 ) ) ;
#144799=CARTESIAN_POINT ( 'NONE',  ( 18.39999999999999503, 5.650000000011139001, -79.65000000000004832 ) ) ;
#144855=CARTESIAN_POINT ( 'NONE',  ( -16.93211319090181632, 9.999986781168624717, -87.92250549927310033 ) ) ;
#145092=CIRCLE ( 'NONE', #228325, 0.1000000000000028644 ) ;
#145156=CARTESIAN_POINT ( 'NONE',  ( -16.77779411440718604, 9.946101447118758543, -87.83694258299551905 ) ) ;
#145193=CARTESIAN_POINT ( 'NONE',  ( 16.87683809663749557, 9.950000000011131718, -87.85000000000005116 ) ) ;
#145245=CARTESIAN_POINT ( 'NONE',  ( -16.80891096016337727, 9.950000000011137047, -87.86766280726713774 ) ) ;
#145537=CARTESIAN_POINT ( 'NONE',  ( -16.85718274719420506, 9.976142314632891583, -87.93665366781755210 ) ) ;
#145646=EDGE_CURVE ( 'NONE', #2598, #81779, #120501, .T. ) ;
#145749=ORIENTED_EDGE ( 'NONE', *, *, #142597, .F. ) ;
#145775=CARTESIAN_POINT ( 'NONE',  ( -21.65000000000000213, 7.250000000011138646, -76.25000000000004263 ) ) ;
#145836=CARTESIAN_POINT ( 'NONE',  ( -18.40000000000000213, 8.822561741677553471, -91.25000000000005684 ) ) ;
#146041=VERTEX_POINT ( 'NONE', #237556 ) ;
#146061=ORIENTED_EDGE ( 'NONE', *, *, #29726, .T. ) ;
#146336=VERTEX_POINT ( 'NONE', #133024 ) ;
#146359=ORIENTED_EDGE ( 'NONE', *, *, #141917, .T. ) ;
#146521=CARTESIAN_POINT ( 'NONE',  ( -16.87998658237752991, 9.950000000011197443, -87.63636043226256334 ) ) ;
#146623=ORIENTED_EDGE ( 'NONE', *, *, #149451, .T. ) ;
#146715=VERTEX_POINT ( 'NONE', #221510 ) ;
#146897=DIRECTION ( 'NONE',  ( 1.000000000000000000, 0.000000000000000000, -0.000000000000000000 ) ) ;
#147190=EDGE_LOOP ( 'NONE', ( #246477, #99631, #53715, #63183 ) ) ;
#147294=CARTESIAN_POINT ( 'NONE',  ( -16.87383368123029825, 9.950000000011138823, -79.65000000000004832 ) ) ;
#147359=VERTEX_POINT ( 'NONE', #161718 ) ;
#147494=DIRECTION ( 'NONE',  ( 1.000000000000000000, 1.186688945009009831E-16, 0.000000000000000000 ) ) ;
#147550=DIRECTION ( 'NONE',  ( -0.000000000000000000, 1.000000000000000000, 0.000000000000000000 ) ) ;
#147590=( BOUNDED_CURVE ( )  B_SPLINE_CURVE ( 3, ( #244247, #143866, #186881, #121772 ),
 .UNSPECIFIED., .F., .F. ) 
 B_SPLINE_CURVE_WITH_KNOTS ( ( 4, 4 ),
 ( 0.3000847527772381729, 0.5497968875596822569 ),
 .UNSPECIFIED. ) 
 CURVE ( )  GEOMETRIC_REPRESENTATION_ITEM ( )  RATIONAL_B_SPLINE_CURVE ( ( 1.000000000000000000, 0.9948104011409419911, 0.9948104011409419911, 1.000000000000000000 ) ) 
 REPRESENTATION_ITEM ( '' )  );
#147862=VECTOR ( 'NONE', #247352, 1000.000000000000000 ) ;
#147880=CARTESIAN_POINT ( 'NONE',  ( -18.40000000000000213, 5.650000000011139001, -79.65000000000004832 ) ) ;
#147914=CARTESIAN_POINT ( 'NONE',  ( -17.05016517656043362, 9.950000000011138823, -79.67269799600136082 ) ) ;
#148636=AXIS2_PLACEMENT_3D ( 'NONE', #229466, #74269, #50793 ) ;
#148939=ADVANCED_FACE ( 'NONE', ( #257580 ), #215930, .F. ) ;
#149158=EDGE_LOOP ( 'NONE', ( #196855, #249535, #187782, #28293 ) ) ;
#149207=CARTESIAN_POINT ( 'NONE',  ( -17.11825945287482753, 9.950000000011138823, -79.75000000000005684 ) ) ;
#149345=CARTESIAN_POINT ( 'NONE',  ( -16.86133551771148831, 9.950000000011137047, -87.80134343454673740 ) ) ;
#149386=CARTESIAN_POINT ( 'NONE',  ( -15.70407651835961005, 9.355806591641286474, -83.29110253154621546 ) ) ;
#149451=EDGE_CURVE ( 'NONE', #3745, #73958, #154112, .T. ) ;
#149515=CARTESIAN_POINT ( 'NONE',  ( -12.68215100488889924, 9.396630376328870327, -84.90705739281833075 ) ) ;
#149529=VECTOR ( 'NONE', #86286, 1000.000000000000000 ) ;
#149544=CARTESIAN_POINT ( 'NONE',  ( -16.89268316805466341, 9.951721813253341153, -79.64424752145448849 ) ) ;
#149551=CARTESIAN_POINT ( 'NONE',  ( -16.88593481969334320, 9.950560090095466492, -87.85187225694454582 ) ) ;
#149786=CARTESIAN_POINT ( 'NONE',  ( -18.40000000000000213, 11.48667500176882861, -91.25000000000005684 ) ) ;
#149819=DIRECTION ( 'NONE',  ( 0.000000000000000000, 0.000000000000000000, 1.000000000000000000 ) ) ;
#149931=DIRECTION ( 'NONE',  ( 1.186688945009009831E-16, -1.000000000000000000, 0.000000000000000000 ) ) ;
#149988=CARTESIAN_POINT ( 'NONE',  ( -17.01764560440454233, 9.950000000011138823, -87.75000000078685503 ) ) ;
#150027=CARTESIAN_POINT ( 'NONE',  ( -16.93521499325732549, 9.994786119814676795, -87.90710854109359218 ) ) ;
#150054=EDGE_CURVE ( 'NONE', #71575, #102037, #28748, .T. ) ;
#150240=CARTESIAN_POINT ( 'NONE',  ( 18.54999999999999716, 8.750000000011182166, -76.25000000000004263 ) ) ;
#150502=CARTESIAN_POINT ( 'NONE',  ( -16.94180778212362881, 9.992443055743304825, -79.60418357053329430 ) ) ;
#150685=CARTESIAN_POINT ( 'NONE',  ( -18.39999999999999858, 11.47867410001043531, -76.27469321634069388 ) ) ;
#150708=VECTOR ( 'NONE', #167605, 1000.000000000000000 ) ;
#151065=ORIENTED_EDGE ( 'NONE', *, *, #138298, .F. ) ;
#151090=PLANE ( 'NONE',  #31996 ) ;
#151465=EDGE_LOOP ( 'NONE', ( #93719, #172288, #10526, #157209, #217602 ) ) ;
#151507=ORIENTED_EDGE ( 'NONE', *, *, #3743, .F. ) ;
#151672=ORIENTED_EDGE ( 'NONE', *, *, #145646, .F. ) ;
#151754=CARTESIAN_POINT ( 'NONE',  ( -17.11825945287481332, 9.950000000011138823, -87.75000000000005684 ) ) ;
#151930=CARTESIAN_POINT ( 'NONE',  ( -18.44085059012131822, 11.51401249349495437, -76.25969468087851055 ) ) ;
#152025=CARTESIAN_POINT ( 'NONE',  ( -16.94445028196808778, 9.992063609708889516, -79.60733017841850767 ) ) ;
#152148=VERTEX_POINT ( 'NONE', #126692 ) ;
#152624=CARTESIAN_POINT ( 'NONE',  ( 15.74999999999999645, 9.350000000011139178, -83.75000000000004263 ) ) ;
#152854=B_SPLINE_CURVE_WITH_KNOTS ( 'NONE', 3,
 ( #227770, #89535, #248621, #70013, #149551, #236745, #18986, #215889, #254972, #98484 ),
 .UNSPECIFIED., .F., .F.,
 ( 4, 3, 3, 4 ),
 ( 0.000000000000000000, 1.004626015991589319E-05, 1.831183478183387304E-05, 2.062343583996250457E-05 ),
 .UNSPECIFIED. ) ;
#152879=AXIS2_PLACEMENT_3D ( 'NONE', #38024, #155416, #137096 ) ;
#152927=EDGE_CURVE ( 'NONE', #232805, #13912, #178111, .T. ) ;
#153221=CARTESIAN_POINT ( 'NONE',  ( -17.22767730082996707, 10.34924421247852422, -78.35757130942955939 ) ) ;
#153315=EDGE_CURVE ( 'NONE', #68524, #32954, #112776, .T. ) ;
#153379=CARTESIAN_POINT ( 'NONE',  ( 20.73486653747088582, 7.250000000011182166, -76.25000000000004263 ) ) ;
#153502=EDGE_LOOP ( 'NONE', ( #127581, #194105, #172603, #69324, #119688, #52056, #209164, #171034, #205922, #239840, #49659, #19248, #74642, #199223, #84144, #191655, #211776, #141169 ) ) ;
#153513=CARTESIAN_POINT ( 'NONE',  ( 0.000000000000000000, 0.000000000000000000, 0.000000000000000000 ) ) ;
#153597=CARTESIAN_POINT ( 'NONE',  ( 20.99999999999999645, 9.750000000011137757, -79.65000000000004832 ) ) ;
#153649=FACE_OUTER_BOUND ( 'NONE', #26039, .T. ) ;
#153771=CIRCLE ( 'NONE', #224439, 1.749999999999998002 ) ;
#153932=CARTESIAN_POINT ( 'NONE',  ( 12.33938619321247998, 9.360723793997191677, -84.31392719460676233 ) ) ;
#154002=B_SPLINE_CURVE_WITH_KNOTS ( 'NONE', 3,
 ( #149544, #213324, #93384, #11294, #36002, #169117, #34731, #154680, #174263, #115514 ),
 .UNSPECIFIED., .F., .F.,
 ( 4, 3, 3, 4 ),
 ( 1.894194122894209342E-15, 3.877043166999333273E-05, 7.336897548476464001E-05, 7.659383120239687261E-05 ),
 .UNSPECIFIED. ) ;
#154112=B_SPLINE_CURVE_WITH_KNOTS ( 'NONE', 3,
 ( #117827, #231376, #202505, #64281, #142514, #219488, #141250, #222036, #434, #23900 ),
 .UNSPECIFIED., .F., .F.,
 ( 4, 2, 2, 2, 4 ),
 ( 0.000000000000000000, 0.0003916577441626962618, 0.0005874866162440451787, 0.0006854010522846982513, 0.0007833154883253513239 ),
 .UNSPECIFIED. ) ;
#154203=B_SPLINE_CURVE_WITH_KNOTS ( 'NONE', 3,
 ( #14484, #215223, #116137, #93979, #90119, #169722, #70611 ),
 .UNSPECIFIED., .F., .F.,
 ( 4, 3, 4 ),
 ( 0.000000000000000000, 3.882884552234470657E-05, 5.798605692158509758E-05 ),
 .UNSPECIFIED. ) ;
#154259=ORIENTED_EDGE ( 'NONE', *, *, #107824, .F. ) ;
#154389=EDGE_LOOP ( 'NONE', ( #76811, #114016, #71748, #163397 ) ) ;
#154647=CARTESIAN_POINT ( 'NONE',  ( -18.38639463286148867, 11.48019957384713230, -76.25000000000004263 ) ) ;
#154680=CARTESIAN_POINT ( 'NONE',  ( -16.94333152886235894, 9.990342011461637028, -79.60796846894562862 ) ) ;
#154767=AXIS2_PLACEMENT_3D ( 'NONE', #105446, #186315, #187611 ) ;
#155123=ORIENTED_EDGE ( 'NONE', *, *, #26669, .F. ) ;
#155195=CARTESIAN_POINT ( 'NONE',  ( 14.88075390448864965, 9.431689550535256927, -85.27929003223610493 ) ) ;
#155242=VERTEX_POINT ( 'NONE', #242704 ) ;
#155416=DIRECTION ( 'NONE',  ( 1.000000000000000000, 0.000000000000000000, 0.000000000000000000 ) ) ;
#155519=AXIS2_PLACEMENT_3D ( 'NONE', #143796, #242902, #220779 ) ;
#155612=CARTESIAN_POINT ( 'NONE',  ( -16.80070461187915498, 9.950000000011140600, -79.64696382916137907 ) ) ;
#155764=CARTESIAN_POINT ( 'NONE',  ( 18.39999999999997371, 11.47316190337362940, -91.25000000000005684 ) ) ;
#156050=ORIENTED_EDGE ( 'NONE', *, *, #126357, .T. ) ;
#156122=CARTESIAN_POINT ( 'NONE',  ( -16.86422026484316916, 9.970447360871810716, -79.58221322567304412 ) ) ;
#156146=ORIENTED_EDGE ( 'NONE', *, *, #180835, .T. ) ;
#156539=ORIENTED_EDGE ( 'NONE', *, *, #129234, .F. ) ;
#156561=ORIENTED_EDGE ( 'NONE', *, *, #11332, .F. ) ;
#156773=LINE ( 'NONE', #38097, #51373 ) ;
#156797=VECTOR ( 'NONE', #206702, 1000.000000000000000 ) ;
#157147=AXIS2_PLACEMENT_3D ( 'NONE', #21250, #202418, #138558 ) ;
#157209=ORIENTED_EDGE ( 'NONE', *, *, #31425, .F. ) ;
#157214=CARTESIAN_POINT ( 'NONE',  ( -18.37160782347004329, 11.47561641481354044, -76.25000000000004263 ) ) ;
#157241=AXIS2_PLACEMENT_3D ( 'NONE', #153597, #253912, #15340 ) ;
#157380=AXIS2_PLACEMENT_3D ( 'NONE', #40924, #175302, #99547 ) ;
#157414=CARTESIAN_POINT ( 'NONE',  ( -16.88495309932521593, 9.954627058484010860, -79.63454867381196323 ) ) ;
#157466=CARTESIAN_POINT ( 'NONE',  ( -16.77683809663752257, 23.65833333334447985, -83.75000000000004263 ) ) ;
#157483=EDGE_CURVE ( 'NONE', #73958, #130466, #182780, .T. ) ;
#157734=DIRECTION ( 'NONE',  ( -0.000000000000000000, 0.000000000000000000, -1.000000000000000000 ) ) ;
#157743=CARTESIAN_POINT ( 'NONE',  ( -16.87036670365548474, 9.989418819312801290, -87.97956011730209980 ) ) ;
#157840=EDGE_CURVE ( 'NONE', #56045, #143848, #114889, .T. ) ;
#157858=AXIS2_PLACEMENT_3D ( 'NONE', #252849, #149931, #14274 ) ;
#158005=VERTEX_POINT ( 'NONE', #5314 ) ;
#158076=DIRECTION ( 'NONE',  ( -0.5932847527679298016, 0.8049926720990051576, 0.000000000000000000 ) ) ;
#158170=DIRECTION ( 'NONE',  ( 0.7071067811865463515, -0.7071067811865487940, 4.930380657631324879E-32 ) ) ;
#158188=CARTESIAN_POINT ( 'NONE',  ( -16.84981964351502626, 9.917318234110023667, -79.86960161401955816 ) ) ;
#158387=CARTESIAN_POINT ( 'NONE',  ( -21.64999999999999858, 10.05000000001113847, -79.75000000000004263 ) ) ;
#158821=SURFACE_STYLE_FILL_AREA ( #224851 ) ;
#158990=ORIENTED_EDGE ( 'NONE', *, *, #137294, .T. ) ;
#159001=DIRECTION ( 'NONE',  ( 1.000000000000000000, 1.186688945009009831E-16, 0.000000000000000000 ) ) ;
#159059=LINE ( 'NONE', #136898, #50602 ) ;
#159408=CARTESIAN_POINT ( 'NONE',  ( -16.81453563122428818, 9.939100205448113456, -87.78825866064536854 ) ) ;
#159441=CARTESIAN_POINT ( 'NONE',  ( -16.87333278164142314, 9.882609784590052016, -80.13316780615271284 ) ) ;
#159461=CARTESIAN_POINT ( 'NONE',  ( -16.81453046979149235, 9.939102281452072418, -79.71172652360306188 ) ) ;
#159532=LINE ( 'NONE', #236480, #198991 ) ;
#159664=CARTESIAN_POINT ( 'NONE',  ( -14.00000000000000178, 9.850000000011133849, -83.75000000000004263 ) ) ;
#159752=CARTESIAN_POINT ( 'NONE',  ( -16.86733706339143524, 9.965990529650820662, -87.90311530199875278 ) ) ;
#159963=CARTESIAN_POINT ( 'NONE',  ( 23.24999999999999645, 5.650000000011139001, -87.85000000000003695 ) ) ;
#159964=ORIENTED_EDGE ( 'NONE', *, *, #167466, .T. ) ;
#160139=ORIENTED_EDGE ( 'NONE', *, *, #160867, .T. ) ;
#160290=CARTESIAN_POINT ( 'NONE',  ( 12.93225390519044460, 9.417651958852157890, -82.35878739244050450 ) ) ;
#160555=DIRECTION ( 'NONE',  ( -1.073024830501117725E-15, 0.000000000000000000, -1.000000000000000000 ) ) ;
#160601=CARTESIAN_POINT ( 'NONE',  ( 18.39999999999999503, 5.650000000011139001, -87.85000000000003695 ) ) ;
#160712=CARTESIAN_POINT ( 'NONE',  ( -16.85939681242905763, 9.905225185936458843, -87.53992195519153086 ) ) ;
#160744=EDGE_CURVE ( 'NONE', #185693, #71575, #240127, .T. ) ;
#160861=CIRCLE ( 'NONE', #194182, 1.749999999999999778 ) ;
#160867=EDGE_CURVE ( 'NONE', #52869, #232805, #109198, .T. ) ;
#161101=CIRCLE ( 'NONE', #148636, 0.5000000000000004441 ) ;
#161213=LINE ( 'NONE', #139028, #220984 ) ;
#161331=VECTOR ( 'NONE', #189303, 1000.000000000000000 ) ;
#161390=ORIENTED_EDGE ( 'NONE', *, *, #208451, .F. ) ;
#161626=EDGE_CURVE ( 'NONE', #52869, #14621, #244993, .T. ) ;
#161709=CARTESIAN_POINT ( 'NONE',  ( -21.65000000000000213, 9.950000000011138823, -79.75000000000004263 ) ) ;
#161713=ORIENTED_EDGE ( 'NONE', *, *, #82807, .F. ) ;
#161718=CARTESIAN_POINT ( 'NONE',  ( 18.39999999999999503, 11.47316190337363828, -87.85000000000003695 ) ) ;
#161771=ORIENTED_EDGE ( 'NONE', *, *, #180539, .T. ) ;
#161987=CARTESIAN_POINT ( 'NONE',  ( -16.79140778683509438, 9.944941598865721488, -87.82973723377084241 ) ) ;
#161993=LINE ( 'NONE', #257157, #244560 ) ;
#162001=CARTESIAN_POINT ( 'NONE',  ( -21.65000000000000213, 9.950000000011140600, -79.65000000000004832 ) ) ;
#162245=EDGE_CURVE ( 'NONE', #1805, #241566, #223995, .T. ) ;
#162278=DIRECTION ( 'NONE',  ( 0.000000000000000000, 0.000000000000000000, 1.000000000000000000 ) ) ;
#162567=CARTESIAN_POINT ( 'NONE',  ( -16.89318236219975589, 9.951535257886286345, -87.85512963210589987 ) ) ;
#162600=CARTESIAN_POINT ( 'NONE',  ( 18.54999999999999716, 23.65833333334447985, -83.75000000000004263 ) ) ;
#162602=VECTOR ( 'NONE', #243433, 1000.000000000000000 ) ;
#162897=CYLINDRICAL_SURFACE ( 'NONE', #48876, 1.749999999999998002 ) ;
#162973=DIRECTION ( 'NONE',  ( -0.000000000000000000, -0.000000000000000000, -1.000000000000000000 ) ) ;
#163027=ORIENTED_EDGE ( 'NONE', *, *, #230407, .T. ) ;
#163147=CARTESIAN_POINT ( 'NONE',  ( -16.92563707711778065, 9.968990694407935393, -87.88075829952403240 ) ) ;
#163397=ORIENTED_EDGE ( 'NONE', *, *, #180835, .F. ) ;
#163851=ORIENTED_EDGE ( 'NONE', *, *, #230407, .F. ) ;
#163916=CARTESIAN_POINT ( 'NONE',  ( -16.94445028196807002, 9.992063609708893068, -87.89266982158160602 ) ) ;
#164014=CARTESIAN_POINT ( 'NONE',  ( 18.39999999999999503, 5.650000000011139001, -79.65000000000004832 ) ) ;
#164122=CARTESIAN_POINT ( 'NONE',  ( 15.52844286134407525, 9.375669526436928081, -82.86779000938595630 ) ) ;
#164540=ADVANCED_FACE ( 'NONE', ( #77660 ), #246619, .T. ) ;
#164684=ORIENTED_EDGE ( 'NONE', *, *, #3886, .F. ) ;
#164806=LINE ( 'NONE', #26592, #136818 ) ;
#164833=CARTESIAN_POINT ( 'NONE',  ( -16.89935556175728948, 9.950000000011137047, -87.36032363711532867 ) ) ;
#165086=CARTESIAN_POINT ( 'NONE',  ( -15.55912972643741199, 8.490870273573719373, -79.55000000000005400 ) ) ;
#165100=CIRCLE ( 'NONE', #132336, 0.09999999999999939493 ) ;
#165104=CARTESIAN_POINT ( 'NONE',  ( -16.77683809663752257, 9.945835743215303282, -87.83605098089584828 ) ) ;
#165117=FACE_OUTER_BOUND ( 'NONE', #20728, .T. ) ;
#165202=FACE_OUTER_BOUND ( 'NONE', #48911, .T. ) ;
#165720=CARTESIAN_POINT ( 'NONE',  ( -16.90987985657661596, 9.957807518190884721, -87.86928708888368078 ) ) ;
#165722=VECTOR ( 'NONE', #239130, 1000.000000000000000 ) ;
#165832=ORIENTED_EDGE ( 'NONE', *, *, #200142, .T. ) ;
#165855=ORIENTED_EDGE ( 'NONE', *, *, #96995, .T. ) ;
#166148=ORIENTED_EDGE ( 'NONE', *, *, #4044, .F. ) ;
#166297=ADVANCED_FACE ( 'NONE', ( #194541 ), #211513, .T. ) ;
#166329=CARTESIAN_POINT ( 'NONE',  ( -33.72168855820451938, 9.950000000011156587, -87.85000000000009379 ) ) ;
#166459=CARTESIAN_POINT ( 'NONE',  ( -33.72168855820452649, 23.65833333334447985, -83.75000000000004263 ) ) ;
#166516=CARTESIAN_POINT ( 'NONE',  ( -15.66061380678752535, 9.360723793997191677, -84.31392719460676233 ) ) ;
#166537=AXIS2_PLACEMENT_3D ( 'NONE', #256728, #157734, #237225 ) ;
#166648=ORIENTED_EDGE ( 'NONE', *, *, #130908, .T. ) ;
#166848=CARTESIAN_POINT ( 'NONE',  ( 20.73486653747088937, 7.750000000011182166, -79.65000000000004832 ) ) ;
#166992=ORIENTED_EDGE ( 'NONE', *, *, #87337, .F. ) ;
#167105=CARTESIAN_POINT ( 'NONE',  ( -18.40000000000000213, 11.75000000001113953, -79.65000000000004832 ) ) ;
#167120=ORIENTED_EDGE ( 'NONE', *, *, #67982, .T. ) ;
#167245=LINE ( 'NONE', #47241, #11713 ) ;
#167279=ORIENTED_EDGE ( 'NONE', *, *, #137294, .F. ) ;
#167294=EDGE_LOOP ( 'NONE', ( #111034, #151065, #187074, #242229 ) ) ;
#167378=ORIENTED_EDGE ( 'NONE', *, *, #61366, .T. ) ;
#167466=EDGE_CURVE ( 'NONE', #2598, #48110, #167632, .T. ) ;
#167605=DIRECTION ( 'NONE',  ( 1.186688945009010077E-16, -1.000000000000000000, -0.000000000000000000 ) ) ;
#167632=LINE ( 'NONE', #103753, #213496 ) ;
#167662=CARTESIAN_POINT ( 'NONE',  ( -14.45443560709636621, 9.450592112144860835, -82.05618831880845221 ) ) ;
#167777=CIRCLE ( 'NONE', #59373, 0.09999999999999939493 ) ;
#167801=CARTESIAN_POINT ( 'NONE',  ( -15.69373346032659811, 9.356790025057039273, -84.20482650861393381 ) ) ;
#167955=PLANE ( 'NONE',  #205355 ) ;
#168075=DIRECTION ( 'NONE',  ( 0.000000000000000000, 0.000000000000000000, 1.000000000000000000 ) ) ;
#168170=AXIS2_PLACEMENT_3D ( 'NONE', #140397, #216085, #62166 ) ;
#168394=CARTESIAN_POINT ( 'NONE',  ( -14.00000000000000178, 9.850000000011133849, -83.75000000000004263 ) ) ;
#168500=COLOUR_RGB ( '', 0.66274510, 0.83137255, 0.94901961) ;
#168692=ORIENTED_EDGE ( 'NONE', *, *, #67982, .F. ) ;
#168796=CARTESIAN_POINT ( 'NONE',  ( -16.27683809663750480, 9.350000000011133849, -76.25000000000004263 ) ) ;
#168855=ORIENTED_EDGE ( 'NONE', *, *, #203629, .F. ) ;
#168969=CARTESIAN_POINT ( 'NONE',  ( -14.56556274378147720, 9.446557523083688679, -82.08994195434594587 ) ) ;
#169094=CARTESIAN_POINT ( 'NONE',  ( -15.75000000000001066, 9.350000000011142731, -83.86426760761615640 ) ) ;
#169117=CARTESIAN_POINT ( 'NONE',  ( -16.93658623642901873, 9.980381671668284937, -79.61190272912924115 ) ) ;
#169206=( NAMED_UNIT ( * ) PLANE_ANGLE_UNIT ( ) SI_UNIT ( $, .RADIAN. ) );
#169214=EDGE_CURVE ( 'NONE', #203569, #1805, #47898, .T. ) ;
#169265=ORIENTED_EDGE ( 'NONE', *, *, #131112, .F. ) ;
#169384=EDGE_LOOP ( 'NONE', ( #192506, #226348, #220106, #127239 ) ) ;
#169521=ORIENTED_EDGE ( 'NONE', *, *, #29363, .T. ) ;
#169573=CARTESIAN_POINT ( 'NONE',  ( -16.93388492042257454, 9.988541822527057690, -87.90054512318621960 ) ) ;
#169623=DIRECTION ( 'NONE',  ( -1.000000000000000000, 1.652117596168391700E-15, 0.000000000000000000 ) ) ;
#169722=CARTESIAN_POINT ( 'NONE',  ( -18.39418127959864790, 11.48390560170929220, -91.25000000000005684 ) ) ;
#169745=ADVANCED_FACE ( 'NONE', ( #91866 ), #110144, .F. ) ;
#170187=EDGE_CURVE ( 'NONE', #198491, #39296, #210248, .T. ) ;
#170401=ADVANCED_FACE ( 'NONE', ( #17186 ), #255731, .F. ) ;
#170519=ORIENTED_EDGE ( 'NONE', *, *, #74619, .T. ) ;
#170692=DIRECTION ( 'NONE',  ( 1.000000000000000000, 1.186688945009010077E-16, 0.000000000000000000 ) ) ;
#170848=VECTOR ( 'NONE', #95741, 1000.000000000000000 ) ;
#170888=VERTEX_POINT ( 'NONE', #102449 ) ;
#170927=CARTESIAN_POINT ( 'NONE',  ( 12.84435279558019261, 9.410708747058235346, -85.06920840584413668 ) ) ;
#171034=ORIENTED_EDGE ( 'NONE', *, *, #91931, .T. ) ;
#171232=( BOUNDED_CURVE ( )  B_SPLINE_CURVE ( 3, ( #198335, #120126, #234910, #219172 ),
 .UNSPECIFIED., .F., .F. ) 
 B_SPLINE_CURVE_WITH_KNOTS ( ( 4, 4 ),
 ( 2.589852378279005940, 2.850972632318389710 ),
 .UNSPECIFIED. ) 
 CURVE ( )  GEOMETRIC_REPRESENTATION_ITEM ( )  RATIONAL_B_SPLINE_CURVE ( ( 1.000000000000000000, 0.9943260843901262636, 0.9943260843901262636, 1.000000000000000000 ) ) 
 REPRESENTATION_ITEM ( '' )  );
#171367=CARTESIAN_POINT ( 'NONE',  ( -17.01764560440328466, 9.950000000011138823, -79.74999999921324445 ) ) ;
#171523=CARTESIAN_POINT ( 'NONE',  ( -13.88555196119803448, 9.457431528860068326, -81.99991693789972658 ) ) ;
#171655=DIRECTION ( 'NONE',  ( 1.000000000000000000, 0.000000000000000000, 0.000000000000000000 ) ) ;
#171660=CARTESIAN_POINT ( 'NONE',  ( -12.42749937872396337, 9.370689921613768902, -84.52646512666109402 ) ) ;
#171691=VERTEX_POINT ( 'NONE', #64041 ) ;
#171710=CARTESIAN_POINT ( 'NONE',  ( -16.77683809663752257, 9.950000000011138823, -87.85000000000005116 ) ) ;
#171964=FACE_OUTER_BOUND ( 'NONE', #197747, .T. ) ;
#172208=CARTESIAN_POINT ( 'NONE',  ( 12.42718393586866732, 9.370655051134638924, -84.52582325598092439 ) ) ;
#172288=ORIENTED_EDGE ( 'NONE', *, *, #180711, .F. ) ;
#172515=VERTEX_POINT ( 'NONE', #145193 ) ;
#172520=LINE ( 'NONE', #232463, #56852 ) ;
#172603=ORIENTED_EDGE ( 'NONE', *, *, #3886, .T. ) ;
#172774=CARTESIAN_POINT ( 'NONE',  ( 17.23472005113827166, 10.30788195451192379, -89.04657686006872552 ) ) ;
#172796=CARTESIAN_POINT ( 'NONE',  ( -16.87036670365549540, 9.989418819312804843, -79.52043988269798547 ) ) ;
#172820=CARTESIAN_POINT ( 'NONE',  ( -14.23072895065543264, 9.455987233623899257, -82.01153116689789613 ) ) ;
#172942=CARTESIAN_POINT ( 'NONE',  ( -18.40000000000000213, 11.48667500176882328, -76.25000000000004263 ) ) ;
#173072=( NAMED_UNIT ( * ) SI_UNIT ( $, .STERADIAN. ) SOLID_ANGLE_UNIT ( ) );
#173498=CARTESIAN_POINT ( 'NONE',  ( 12.26145404764308644, 9.351413679112543065, -83.98034356754899932 ) ) ;
#173508=FACE_OUTER_BOUND ( 'NONE', #103223, .T. ) ;
#173906=PRODUCT_DEFINITION_FORMATION_WITH_SPECIFIED_SOURCE ( 'ANY', '', #257766, .NOT_KNOWN. ) ;
#173916=AXIS2_PLACEMENT_3D ( 'NONE', #116852, #196378, #138941 ) ;
#173926=CARTESIAN_POINT ( 'NONE',  ( -16.91256925476571027, 9.985731158139330432, -79.53235751099477113 ) ) ;
#173961=CARTESIAN_POINT ( 'NONE',  ( -16.94062896051973865, 9.992719105111833144, -79.60251654211884897 ) ) ;
#174204=DIRECTION ( 'NONE',  ( 0.000000000000000000, 0.000000000000000000, -1.000000000000000000 ) ) ;
#174263=CARTESIAN_POINT ( 'NONE',  ( -16.94389599338512298, 9.991197989766199328, -79.60764480181029512 ) ) ;
#174277=FACE_OUTER_BOUND ( 'NONE', #247471, .T. ) ;
#174357=SHAPE_REPRESENTATION_RELATIONSHIP ( 'NONE' , 'NONE' ,  #18588, #132074 ) ;
#174595=AXIS2_PLACEMENT_3D ( 'NONE', #254223, #191738, #54751 ) ;
#174677=ORIENTED_EDGE ( 'NONE', *, *, #11065, .T. ) ;
#174775=CARTESIAN_POINT ( 'NONE',  ( 12.30626653967340900, 9.356790025057035720, -84.20482650861391960 ) ) ;
#174782=CYLINDRICAL_SURFACE ( 'NONE', #220509, 1.749999999999999778 ) ;
#175043=DIRECTION ( 'NONE',  ( 0.000000000000000000, 0.000000000000000000, 1.000000000000000000 ) ) ;
#175274=VERTEX_POINT ( 'NONE', #74088 ) ;
#175302=DIRECTION ( 'NONE',  ( -1.000000000000000000, 0.000000000000000000, 0.000000000000000000 ) ) ;
#175318=ADVANCED_FACE ( 'NONE', ( #153649 ), #96163, .T. ) ;
#175457=CARTESIAN_POINT ( 'NONE',  ( -23.25000000000000355, 5.650000000011139001, -76.25000000000004263 ) ) ;
#175484=FACE_OUTER_BOUND ( 'NONE', #130370, .T. ) ;
#175621=ORIENTED_EDGE ( 'NONE', *, *, #74619, .F. ) ;
#175665=LINE ( 'NONE', #92250, #139685 ) ;
#175970=CARTESIAN_POINT ( 'NONE',  ( -23.25000000000000355, 5.650000000011139001, -87.85000000000003695 ) ) ;
#176224=VECTOR ( 'NONE', #196207, 1000.000000000000000 ) ;
#176408=VECTOR ( 'NONE', #44450, 999.9999999999998863 ) ;
#176426=VECTOR ( 'NONE', #87922, 1000.000000000000000 ) ;
#176495=ORIENTED_EDGE ( 'NONE', *, *, #29363, .F. ) ;
#176586=AXIS2_PLACEMENT_3D ( 'NONE', #247433, #187488, #227878 ) ;
#176739=CARTESIAN_POINT ( 'NONE',  ( -16.77732147278574715, 9.945966932584587639, -79.66350875687584221 ) ) ;
#176792=VERTEX_POINT ( 'NONE', #190415 ) ;
#176902=ORIENTED_EDGE ( 'NONE', *, *, #121254, .F. ) ;
#177061=ADVANCED_FACE ( 'NONE', ( #221487 ), #81960, .T. ) ;
#177439=CARTESIAN_POINT ( 'NONE',  ( -20.65000000000000568, 7.250000000011138646, -79.65000000000004832 ) ) ;
#177673=ORIENTED_EDGE ( 'NONE', *, *, #25746, .F. ) ;
#177735=CARTESIAN_POINT ( 'NONE',  ( -16.97683809663752186, 9.950000000011137047, -80.40236401819653622 ) ) ;
#177751=CARTESIAN_POINT ( 'NONE',  ( -17.11825945287482753, 9.950000000011138823, -79.75000000000004263 ) ) ;
#177789=EDGE_CURVE ( 'NONE', #228775, #134584, #165100, .T. ) ;
#177843=VERTEX_POINT ( 'NONE', #107352 ) ;
#177887=CARTESIAN_POINT ( 'NONE',  ( -21.65000000000000213, 7.250000000011138646, -76.25000000000004263 ) ) ;
#177894=CARTESIAN_POINT ( 'NONE',  ( 21.13736287352038445, 8.046642376395153562, -76.25000000000004263 ) ) ;
#177929=DIRECTION ( 'NONE',  ( -1.000000000000000000, 1.652117596168391700E-15, 0.000000000000000000 ) ) ;
#178090=CARTESIAN_POINT ( 'NONE',  ( -18.37013991200266005, 11.49974761622313224, -91.29302301051716029 ) ) ;
#178098=DIRECTION ( 'NONE',  ( 1.000000000000000000, 0.000000000000000000, 0.000000000000000000 ) ) ;
#178111=( BOUNDED_CURVE ( )  B_SPLINE_CURVE ( 3, ( #163916, #243442, #240889, #123504 ),
 .UNSPECIFIED., .F., .F. ) 
 B_SPLINE_CURVE_WITH_KNOTS ( ( 4, 4 ),
 ( 3.752122642744613046, 4.712388980384671910 ),
 .UNSPECIFIED. ) 
 CURVE ( )  GEOMETRIC_REPRESENTATION_ITEM ( )  RATIONAL_B_SPLINE_CURVE ( ( 1.000000000000000000, 0.9246222802177266331, 0.9246222802177266331, 1.000000000000000000 ) ) 
 REPRESENTATION_ITEM ( '' )  );
#178194=ORIENTED_EDGE ( 'NONE', *, *, #238036, .T. ) ;
#178257=VECTOR ( 'NONE', #136949, 1000.000000000000000 ) ;
#178385=( NAMED_UNIT ( * ) SI_UNIT ( $, .STERADIAN. ) SOLID_ANGLE_UNIT ( ) );
#178435=AXIS2_PLACEMENT_3D ( 'NONE', #122219, #103905, #28285 ) ;
#178469=ORIENTED_EDGE ( 'NONE', *, *, #99325, .T. ) ;
#178666=CARTESIAN_POINT ( 'NONE',  ( -17.78043020864320667, 10.85359211201684637, -90.16304916572026684 ) ) ;
#178920=VECTOR ( 'NONE', #218264, 1000.000000000000000 ) ;
#178973=( BOUNDED_CURVE ( )  B_SPLINE_CURVE ( 3, ( #223162, #25003, #104482, #198473 ),
 .UNSPECIFIED., .F., .F. ) 
 B_SPLINE_CURVE_WITH_KNOTS ( ( 4, 4 ),
 ( 1.570796326794885012, 3.141592653589794448 ),
 .UNSPECIFIED. ) 
 CURVE ( )  GEOMETRIC_REPRESENTATION_ITEM ( )  RATIONAL_B_SPLINE_CURVE ( ( 1.000000000000000000, 0.8047378541243619399, 0.8047378541243619399, 1.000000000000000000 ) ) 
 REPRESENTATION_ITEM ( '' )  );
#179009=LINE ( 'NONE', #79839, #2435 ) ;
#179054=CARTESIAN_POINT ( 'NONE',  ( -16.77683809663752257, 9.945835743215301505, -79.66394901910425119 ) ) ;
#179186=CARTESIAN_POINT ( 'NONE',  ( -21.65000000000000213, 10.05000000001113847, -87.85000000000003695 ) ) ;
#179200=CIRCLE ( 'NONE', #229063, 14.30833333333333890 ) ;
#179340=DIRECTION ( 'NONE',  ( 0.000000000000000000, 0.9553114395362780620, -0.2956011730205483912 ) ) ;
#179386=ORIENTED_EDGE ( 'NONE', *, *, #137908, .T. ) ;
#179840=CARTESIAN_POINT ( 'NONE',  ( 13.54556439290363379, 9.450592112144859058, -82.05618831880843800 ) ) ;
#180127=CARTESIAN_POINT ( 'NONE',  ( -17.04761207306820125, 10.02645087340892971, -79.65000000000004832 ) ) ;
#180141=CARTESIAN_POINT ( 'NONE',  ( -16.94333152882355975, 9.990342011468824168, -87.89203153110153721 ) ) ;
#180285=LINE ( 'NONE', #119033, #256100 ) ;
#180355=VECTOR ( 'NONE', #141870, 1000.000000000000000 ) ;
#180393=EDGE_CURVE ( 'NONE', #5367, #14621, #198404, .T. ) ;
#180539=EDGE_CURVE ( 'NONE', #232805, #17316, #128363, .T. ) ;
#180642=CARTESIAN_POINT ( 'NONE',  ( -17.80356949363834218, 10.87673139701198011, -90.21307302422357566 ) ) ;
#180646=AXIS2_PLACEMENT_3D ( 'NONE', #192445, #174204, #136284 ) ;
#180708=APPLICATION_CONTEXT ( 'automotive_design' ) ;
#180711=EDGE_CURVE ( 'NONE', #241355, #143362, #198625, .T. ) ;
#180835=EDGE_CURVE ( 'NONE', #74064, #38688, #252862, .T. ) ;
#180964=ORIENTED_EDGE ( 'NONE', *, *, #30682, .T. ) ;
#181543=CARTESIAN_POINT ( 'NONE',  ( -16.87683809663752399, 9.850000000011144508, -87.09763598180374800 ) ) ;
#181633=VERTEX_POINT ( 'NONE', #2787 ) ;
#181641=ORIENTED_EDGE ( 'NONE', *, *, #252492, .F. ) ;
#181820=ORIENTED_EDGE ( 'NONE', *, *, #6574, .T. ) ;
#182348=CARTESIAN_POINT ( 'NONE',  ( 20.99999999999999645, 9.750000000011137757, -87.85000000000003695 ) ) ;
#182524=CARTESIAN_POINT ( 'NONE',  ( 21.72449340488910607, 10.28395627750227703, -76.25000000000004263 ) ) ;
#182713=CARTESIAN_POINT ( 'NONE',  ( -16.90128866880176517, 9.953795777214113016, -87.86267618338868601 ) ) ;
#182780=B_SPLINE_CURVE_WITH_KNOTS ( 'NONE', 3,
 ( #248549, #30818, #234118, #69941, #134997, #214554, #129876, #119323, #256186, #121902, #138838, #176739, #220970 ),
 .UNSPECIFIED., .F., .F.,
 ( 4, 3, 3, 3, 4 ),
 ( 1.084999851846394431E-16, 1.946463881814305957E-05, 3.922356109944007726E-05, 4.215060953238855979E-05, 4.415117091092329025E-05 ),
 .UNSPECIFIED. ) ;
#183025=CARTESIAN_POINT ( 'NONE',  ( -21.64999999999999858, 9.350000000011133849, -76.25000000000004263 ) ) ;
#183115=CARTESIAN_POINT ( 'NONE',  ( -16.82542659449980604, 9.934499891438555608, -87.75536439997381422 ) ) ;
#183120=FACE_OUTER_BOUND ( 'NONE', #8234, .T. ) ;
#183258=EDGE_CURVE ( 'NONE', #112749, #5367, #239944, .T. ) ;
#183314=ORIENTED_EDGE ( 'NONE', *, *, #169214, .F. ) ;
#183390=VECTOR ( 'NONE', #223962, 1000.000000000000000 ) ;
#183439=EDGE_CURVE ( 'NONE', #158005, #74064, #104991, .T. ) ;
#183467=FACE_OUTER_BOUND ( 'NONE', #105329, .T. ) ;
#183598=ORIENTED_EDGE ( 'NONE', *, *, #135640, .F. ) ;
#183898=ORIENTED_EDGE ( 'NONE', *, *, #91308, .F. ) ;
#183911=CARTESIAN_POINT ( 'NONE',  ( -33.72168855820451938, 9.950000000011156587, -79.65000000000000568 ) ) ;
#183967=DIRECTION ( 'NONE',  ( -0.8049926720990042694, -0.5932847527679310229, 0.000000000000000000 ) ) ;
#183976=CARTESIAN_POINT ( 'NONE',  ( -16.91776028072577631, 9.963400393640901243, -87.87502401470217706 ) ) ;
#184393=ORIENTED_EDGE ( 'NONE', *, *, #131112, .T. ) ;
#184469=LINE ( 'NONE', #241881, #176426 ) ;
#184527=LINE ( 'NONE', #205368, #43599 ) ;
#184992=EDGE_CURVE ( 'NONE', #155242, #176792, #202228, .T. ) ;
#185121=VERTEX_POINT ( 'NONE', #10453 ) ;
#185256=CARTESIAN_POINT ( 'NONE',  ( -23.25000000000000355, 5.650000000011139001, -79.65000000000004832 ) ) ;
#185584=CARTESIAN_POINT ( 'NONE',  ( -16.77732147262506146, 9.945966932629787038, -87.83649124327591551 ) ) ;
#185586=ORIENTED_EDGE ( 'NONE', *, *, #191024, .F. ) ;
#185693=VERTEX_POINT ( 'NONE', #58226 ) ;
#185884=DIRECTION ( 'NONE',  ( 0.000000000000000000, -1.000000000000000000, 0.000000000000000000 ) ) ;
#185985=DIRECTION ( 'NONE',  ( 0.000000000000000000, 0.000000000000000000, -1.000000000000000000 ) ) ;
#186037=VECTOR ( 'NONE', #100851, 1000.000000000000000 ) ;
#186053=CARTESIAN_POINT ( 'NONE',  ( -15.06720934482788188, 9.417690691074263043, -85.14160069676464104 ) ) ;
#186190=DIRECTION ( 'NONE',  ( 1.073024830501117725E-15, -0.000000000000000000, -1.000000000000000000 ) ) ;
#186292=CARTESIAN_POINT ( 'NONE',  ( -18.40000000000000213, 11.33174054713633261, -87.85000000000003695 ) ) ;
#186315=DIRECTION ( 'NONE',  ( -0.7071067811865487940, 0.7071067811865463515, 0.000000000000000000 ) ) ;
#186585=DIRECTION ( 'NONE',  ( 0.000000000000000000, -1.000000000000000000, 0.000000000000000000 ) ) ;
#186663=ORIENTED_EDGE ( 'NONE', *, *, #206925, .F. ) ;
#186706=VECTOR ( 'NONE', #219258, 1000.000000000000000 ) ;
#186783=ORIENTED_EDGE ( 'NONE', *, *, #49510, .T. ) ;
#186881=CARTESIAN_POINT ( 'NONE',  ( -17.78043020864320667, 10.85359211201683927, -77.33695083427984684 ) ) ;
#187000=VERTEX_POINT ( 'NONE', #103808 ) ;
#187074=ORIENTED_EDGE ( 'NONE', *, *, #137908, .F. ) ;
#187160=LINE ( 'NONE', #166329, #156797 ) ;
#187349=PLANE ( 'NONE',  #53920 ) ;
#187425=DIRECTION ( 'NONE',  ( -0.000000000000000000, -0.000000000000000000, -1.000000000000000000 ) ) ;
#187488=DIRECTION ( 'NONE',  ( -1.000000000000000000, -1.186688945009010077E-16, -0.000000000000000000 ) ) ;
#187516=CARTESIAN_POINT ( 'NONE',  ( 18.39999999999999503, 5.650000000011139001, -79.65000000000004832 ) ) ;
#187611=DIRECTION ( 'NONE',  ( 0.000000000000000000, 0.000000000000000000, 1.000000000000000000 ) ) ;
#187730=CARTESIAN_POINT ( 'NONE',  ( -16.87487986503753845, 9.950007555096753720, -79.64997473968678321 ) ) ;
#187751=ORIENTED_EDGE ( 'NONE', *, *, #87597, .F. ) ;
#187782=ORIENTED_EDGE ( 'NONE', *, *, #135640, .T. ) ;
#188167=ORIENTED_EDGE ( 'NONE', *, *, #188663, .F. ) ;
#188277=CARTESIAN_POINT ( 'NONE',  ( -16.87331047859649757, 9.950000000011138823, -87.85000000000005116 ) ) ;
#188440=CARTESIAN_POINT ( 'NONE',  ( -16.94226253665224391, 9.950000000011135270, -87.55326540438426264 ) ) ;
#188469=ORIENTED_EDGE ( 'NONE', *, *, #184992, .F. ) ;
#188608=CARTESIAN_POINT ( 'NONE',  ( -12.26136940704871670, 9.351403174152810749, -83.97953043683850183 ) ) ;
#188663=EDGE_CURVE ( 'NONE', #49816, #32954, #179009, .T. ) ;
#188690=DIRECTION ( 'NONE',  ( 1.000000000000000000, -0.000000000000000000, -0.000000000000000000 ) ) ;
#189077=VECTOR ( 'NONE', #219649, 1000.000000000000000 ) ;
#189121=ORIENTED_EDGE ( 'NONE', *, *, #203075, .T. ) ;
#189133=CARTESIAN_POINT ( 'NONE',  ( -16.93589915522259304, 10.00862525870701170, -87.94056010196035800 ) ) ;
#189284=VECTOR ( 'NONE', #227220, 1000.000000000000000 ) ;
#189303=DIRECTION ( 'NONE',  ( 0.000000000000000000, 0.000000000000000000, 1.000000000000000000 ) ) ;
#189478=EDGE_LOOP ( 'NONE', ( #107854, #116393, #19080, #26605 ) ) ;
#189651=ORIENTED_EDGE ( 'NONE', *, *, #257457, .T. ) ;
#189689=DIRECTION ( 'NONE',  ( -1.000000000000000000, 0.000000000000000000, 0.000000000000000000 ) ) ;
#189745=CARTESIAN_POINT ( 'NONE',  ( -17.29838795458690726, 10.37154985796053452, -78.39525871738324270 ) ) ;
#189769=CARTESIAN_POINT ( 'NONE',  ( -15.75000000000000355, 9.350000000011140955, -83.75000000000004263 ) ) ;
#189866=VERTEX_POINT ( 'NONE', #177751 ) ;
#189899=ADVANCED_FACE ( 'NONE', ( #43358 ), #99443, .T. ) ;
#190415=CARTESIAN_POINT ( 'NONE',  ( 21.72449340488910252, 10.28395627750227703, -79.65000000000004832 ) ) ;
#190931=CARTESIAN_POINT ( 'NONE',  ( -16.93658211146646408, 9.994108662352344297, -79.59570493004436287 ) ) ;
#191024=EDGE_CURVE ( 'NONE', #129272, #206025, #164806, .T. ) ;
#191079=CARTESIAN_POINT ( 'NONE',  ( -12.25000000000000178, 9.350000000011139178, -83.75000000000004263 ) ) ;
#191211=EDGE_LOOP ( 'NONE', ( #113715, #209865, #207087 ) ) ;
#191214=CARTESIAN_POINT ( 'NONE',  ( -12.92414019175886253, 9.417632963117446465, -85.14894846573231746 ) ) ;
#191655=ORIENTED_EDGE ( 'NONE', *, *, #257457, .F. ) ;
#191730=LINE ( 'NONE', #74354, #50730 ) ;
#191738=DIRECTION ( 'NONE',  ( 1.073024830501117725E-15, -0.000000000000000000, -1.000000000000000000 ) ) ;
#191754=CARTESIAN_POINT ( 'NONE',  ( 15.74999999999999645, 9.350000000011133849, -83.86574316727394773 ) ) ;
#191830=AXIS2_PLACEMENT_3D ( 'NONE', #84701, #144701, #3926 ) ;
#191913=AXIS2_PLACEMENT_3D ( 'NONE', #20254, #240576, #179340 ) ;
#192240=CARTESIAN_POINT ( 'NONE',  ( 18.39999999999999503, 11.75000000001113953, -79.65000000000004832 ) ) ;
#192340=CARTESIAN_POINT ( 'NONE',  ( -14.77738660682463667, 9.436552840015579591, -82.17795547276035961 ) ) ;
#192428=CARTESIAN_POINT ( 'NONE',  ( -16.87331047859651179, 9.950000000011142376, -79.65000000000004832 ) ) ;
#192445=CARTESIAN_POINT ( 'NONE',  ( -16.97683809663752186, 9.850000000011140955, -79.65000000000004832 ) ) ;
#192506=ORIENTED_EDGE ( 'NONE', *, *, #51435, .F. ) ;
#192590=DIRECTION ( 'NONE',  ( 1.000000000000000000, 0.000000000000000000, 0.000000000000000000 ) ) ;
#192660=CARTESIAN_POINT ( 'NONE',  ( -16.86757978335471719, 9.965650379045438712, -79.59800465316754980 ) ) ;
#192745=VECTOR ( 'NONE', #142376, 1000.000000000000000 ) ;
#193236=ORIENTED_EDGE ( 'NONE', *, *, #221811, .T. ) ;
#193376=ORIENTED_EDGE ( 'NONE', *, *, #48963, .T. ) ;
#193747=CARTESIAN_POINT ( 'NONE',  ( -18.35235881385853318, 11.47341900772405054, -76.25000000000004263 ) ) ;
#193856=CARTESIAN_POINT ( 'NONE',  ( 16.27683809663749770, 9.350000000011137402, -76.25000000000005684 ) ) ;
#193866=ORIENTED_EDGE ( 'NONE', *, *, #250046, .F. ) ;
#194099=CYLINDRICAL_SURFACE ( 'NONE', #22804, 0.9000000000000014655 ) ;
#194104=AXIS2_PLACEMENT_3D ( 'NONE', #187516, #8859, #88362 ) ;
#194105=ORIENTED_EDGE ( 'NONE', *, *, #74206, .T. ) ;
#194182=AXIS2_PLACEMENT_3D ( 'NONE', #159664, #55380, #76255 ) ;
#194315=CARTESIAN_POINT ( 'NONE',  ( 13.88638282980484639, 9.457426452500058645, -85.50004186840010334 ) ) ;
#194396=CARTESIAN_POINT ( 'NONE',  ( -17.11825945287481332, 10.05000000001113847, -87.85000000000003695 ) ) ;
#194541=FACE_OUTER_BOUND ( 'NONE', #169384, .T. ) ;
#194726=CARTESIAN_POINT ( 'NONE',  ( -16.89155683852514400, 9.950000000011138823, -80.27737184954051486 ) ) ;
#194746=VERTEX_POINT ( 'NONE', #54457 ) ;
#194970=FACE_OUTER_BOUND ( 'NONE', #14073, .T. ) ;
#195039=CARTESIAN_POINT ( 'NONE',  ( -16.86337532320261090, 9.979967204235514089, -87.94892446898285243 ) ) ;
#195184=FILL_AREA_STYLE_COLOUR ( '', #256260 ) ;
#195407=CIRCLE ( 'NONE', #174595, 0.9000000000000014655 ) ;
#195468=DIRECTION ( 'NONE',  ( 0.000000000000000000, 0.000000000000000000, -1.000000000000000000 ) ) ;
#195595=CARTESIAN_POINT ( 'NONE',  ( 12.93279065517212878, 9.417690691074257714, -85.14160069676461262 ) ) ;
#195776=CARTESIAN_POINT ( 'NONE',  ( -33.72168855820452649, 11.47316190337362585, -76.25000000000004263 ) ) ;
#195998=CARTESIAN_POINT ( 'NONE',  ( -16.85697194749131711, 9.908543714134740554, -79.93500426761436017 ) ) ;
#196207=DIRECTION ( 'NONE',  ( -1.020425574104004196E-15, -0.000000000000000000, -1.000000000000000000 ) ) ;
#196313=ORIENTED_EDGE ( 'NONE', *, *, #10382, .T. ) ;
#196378=DIRECTION ( 'NONE',  ( 0.7071067811865487940, 0.7071067811865462405, -7.215498431451186046E-16 ) ) ;
#196450=CARTESIAN_POINT ( 'NONE',  ( -17.11825945287481687, 9.950000000011138823, -87.75000000000004263 ) ) ;
#196632=DIRECTION ( 'NONE',  ( -1.000000000000000000, 0.000000000000000000, 0.000000000000000000 ) ) ;
#196855=ORIENTED_EDGE ( 'NONE', *, *, #111805, .F. ) ;
#197264=CARTESIAN_POINT ( 'NONE',  ( -16.77431908686106610, 9.945805754529134290, -79.66416078234981057 ) ) ;
#197353=B_SPLINE_CURVE_WITH_KNOTS ( 'NONE', 3,
 ( #189769, #91947, #149386, #128516, #132360, #11137, #33304, #112804, #192340, #168969, #167662, #172820, #12439, #171523, #211917, #231479, #108937, #51508, #251001, #252290, #69845, #89366, #93226, #34566, #228901, #191079 ),
 .UNSPECIFIED., .F., .F.,
 ( 4, 2, 2, 2, 2, 2, 2, 2, 2, 2, 2, 2, 4 ),
 ( 0.005476422646581353450, 0.006160811967703566129, 0.006845201288825777074, 0.007187395949386882546, 0.007529590609947988886, 0.007871785270509093491, 0.008213979931070199830, 0.008556174591631306170, 0.008898369252192410775, 0.009240563912753517115, 0.009582758573314621720, 0.01026714789443683440, 0.01095153721555904534 ),
 .UNSPECIFIED. ) ;
#197366=ORIENTED_EDGE ( 'NONE', *, *, #89503, .T. ) ;
#197609=MANIFOLD_SOLID_BREP ( 'Stock-MAS-200-1', #99032 ) ;
#197622=CARTESIAN_POINT ( 'NONE',  ( -18.44085059012131822, 11.51401249349495970, -91.24030531912158892 ) ) ;
#197629=CYLINDRICAL_SURFACE ( 'NONE', #135945, 1.749999999999998002 ) ;
#197710=( LENGTH_UNIT ( ) NAMED_UNIT ( * ) SI_UNIT ( .MILLI., .METRE. ) );
#197722=LINE ( 'NONE', #42495, #224908 ) ;
#197747=EDGE_LOOP ( 'NONE', ( #22260, #9177 ) ) ;
#197877=DIRECTION ( 'NONE',  ( 0.000000000000000000, -1.000000000000000000, 0.000000000000000000 ) ) ;
#197885=ORIENTED_EDGE ( 'NONE', *, *, #230278, .T. ) ;
#197952=DIRECTION ( 'NONE',  ( -0.000000000000000000, -0.000000000000000000, -1.000000000000000000 ) ) ;
#198150=VECTOR ( 'NONE', #239486, 1000.000000000000000 ) ;
#198335=CARTESIAN_POINT ( 'NONE',  ( 18.39999999999998082, 11.47316190337362585, -76.25000000000004263 ) ) ;
#198385=VECTOR ( 'NONE', #88573, 1000.000000000000000 ) ;
#198404=LINE ( 'NONE', #193, #8171 ) ;
#198473=CARTESIAN_POINT ( 'NONE',  ( -18.40000000000000213, 11.47316190337362762, -79.55000000000005400 ) ) ;
#198480=CARTESIAN_POINT ( 'NONE',  ( 20.09999999999999787, 9.750000000011137757, -87.85000000000003695 ) ) ;
#198491=VERTEX_POINT ( 'NONE', #186292 ) ;
#198571=CARTESIAN_POINT ( 'NONE',  ( -16.85939591225059075, 9.905226478399002943, -79.96006824646910616 ) ) ;
#198625=( BOUNDED_CURVE ( )  B_SPLINE_CURVE ( 3, ( #157743, #79415, #216373, #53458 ),
 .UNSPECIFIED., .F., .F. ) 
 B_SPLINE_CURVE_WITH_KNOTS ( ( 4, 4 ),
 ( 0.3000847527772385614, 0.5517402753107881752 ),
 .UNSPECIFIED. ) 
 CURVE ( )  GEOMETRIC_REPRESENTATION_ITEM ( )  RATIONAL_B_SPLINE_CURVE ( ( 1.000000000000000000, 0.9947294176030464508, 0.9947294176030464508, 1.000000000000000000 ) ) 
 REPRESENTATION_ITEM ( '' )  );
#198649=ORIENTED_EDGE ( 'NONE', *, *, #21518, .T. ) ;
#198677=FACE_OUTER_BOUND ( 'NONE', #52305, .T. ) ;
#198717=DIRECTION ( 'NONE',  ( -1.000000000000000000, -0.000000000000000000, -0.000000000000000000 ) ) ;
#198796=CARTESIAN_POINT ( 'NONE',  ( -16.97683809663752186, 9.850000000011137402, -80.40236401819653622 ) ) ;
#198866=CARTESIAN_POINT ( 'NONE',  ( -16.87304349924914604, 9.961745077968330975, -87.88906667504529935 ) ) ;
#198991=VECTOR ( 'NONE', #239059, 1000.000000000000000 ) ;
#199040=VERTEX_POINT ( 'NONE', #198480 ) ;
#199082=ORIENTED_EDGE ( 'NONE', *, *, #21597, .F. ) ;
#199113=DIRECTION ( 'NONE',  ( -0.7071067811865463515, 0.7071067811865487940, -0.000000000000000000 ) ) ;
#199171=CARTESIAN_POINT ( 'NONE',  ( -23.25000000000000355, 9.950000000011138823, -76.25000000000004263 ) ) ;
#199223=ORIENTED_EDGE ( 'NONE', *, *, #89503, .F. ) ;
#199408=CARTESIAN_POINT ( 'NONE',  ( 13.43443725621852458, 9.446557523083688679, -82.08994195434591745 ) ) ;
#199411=CIRCLE ( 'NONE', #86927, 0.5000000000000004441 ) ;
#199595=DIRECTION ( 'NONE',  ( 0.000000000000000000, -0.9553114395362780620, -0.2956011730205483912 ) ) ;
#199749=LINE ( 'NONE', #101877, #217065 ) ;
#199923=ORIENTED_EDGE ( 'NONE', *, *, #21518, .F. ) ;
#200142=EDGE_CURVE ( 'NONE', #42422, #233341, #35939, .T. ) ;
#200327=EDGE_LOOP ( 'NONE', ( #48010, #139335, #113632, #169521 ) ) ;
#200432=ADVANCED_FACE ( 'NONE', ( #246954 ), #68336, .F. ) ;
#200662=ADVANCED_FACE ( 'NONE', ( #66413 ), #151090, .T. ) ;
#200669=DIRECTION ( 'NONE',  ( 1.186688945009009831E-16, -1.000000000000000000, 0.000000000000000000 ) ) ;
#200727=SHAPE_DEFINITION_REPRESENTATION ( #82997, #18588 ) ;
#201144=CARTESIAN_POINT ( 'NONE',  ( -16.87372386987899020, 9.880600233647912845, -80.14926987186645135 ) ) ;
#201212=VERTEX_POINT ( 'NONE', #201443 ) ;
#201374=CARTESIAN_POINT ( 'NONE',  ( -16.87683809663752399, 9.850000000011139178, -87.09763598180373378 ) ) ;
#201443=CARTESIAN_POINT ( 'NONE',  ( -20.65000000000000568, 5.650000000011139001, -79.65000000000004832 ) ) ;
#201517=EDGE_CURVE ( 'NONE', #38688, #74064, #95793, .T. ) ;
#201550=AXIS2_PLACEMENT_3D ( 'NONE', #227517, #189689, #107569 ) ;
#201934=AXIS2_PLACEMENT_3D ( 'NONE', #144799, #160555, #83524 ) ;
#202066=EDGE_CURVE ( 'NONE', #199040, #248456, #15988, .T. ) ;
#202228=LINE ( 'NONE', #46978, #176408 ) ;
#202263=CARTESIAN_POINT ( 'NONE',  ( -16.94389599337535657, 9.991197989767881538, -87.89235519820165621 ) ) ;
#202418=DIRECTION ( 'NONE',  ( -0.000000000000000000, -0.000000000000000000, -1.000000000000000000 ) ) ;
#202505=CARTESIAN_POINT ( 'NONE',  ( -16.97048326478264002, 9.950000000011133494, -80.14110688012718242 ) ) ;
#202577=CARTESIAN_POINT ( 'NONE',  ( 12.25000000000000000, 9.350000000011140955, -83.75000000000004263 ) ) ;
#202839=ORIENTED_EDGE ( 'NONE', *, *, #111779, .T. ) ;
#202976=FACE_BOUND ( 'NONE', #86786, .T. ) ;
#203075=EDGE_CURVE ( 'NONE', #147359, #187000, #143572, .T. ) ;
#203252=DIRECTION ( 'NONE',  ( -0.000000000000000000, 1.000000000000000000, 0.000000000000000000 ) ) ;
#203322=CARTESIAN_POINT ( 'NONE',  ( -16.77683809663752257, 23.65833333334447985, -83.75000000000004263 ) ) ;
#203535=FACE_OUTER_BOUND ( 'NONE', #118810, .T. ) ;
#203569=VERTEX_POINT ( 'NONE', #67252 ) ;
#203629=EDGE_CURVE ( 'NONE', #67043, #102764, #197353, .T. ) ;
#203800=EDGE_CURVE ( 'NONE', #146336, #59523, #121802, .T. ) ;
#203847=DIRECTION ( 'NONE',  ( -1.000000000000000000, 1.652117596168391700E-15, 0.000000000000000000 ) ) ;
#203946=CARTESIAN_POINT ( 'NONE',  ( -16.87401514999228525, 9.950000000011137047, -87.78001799253213733 ) ) ;
#203980=ADVANCED_FACE ( 'NONE', ( #48658 ), #248152, .F. ) ;
#204484=ADVANCED_FACE ( 'NONE', ( #173508 ), #174782, .F. ) ;
#204529=LINE ( 'NONE', #145836, #99844 ) ;
#204859=EDGE_CURVE ( 'NONE', #130466, #241566, #179200, .T. ) ;
#205214=CARTESIAN_POINT ( 'NONE',  ( -16.85722902420147662, 9.950000000011105072, -87.73445252622929047 ) ) ;
#205282=FILL_AREA_STYLE_COLOUR ( '', #168500 ) ;
#205331=EDGE_CURVE ( 'NONE', #229007, #214712, #131569, .T. ) ;
#205355=AXIS2_PLACEMENT_3D ( 'NONE', #145775, #8853, #208356 ) ;
#205368=CARTESIAN_POINT ( 'NONE',  ( -17.01825945287482966, 10.05000000001113847, -79.65000000000004832 ) ) ;
#205369=ORIENTED_EDGE ( 'NONE', *, *, #245974, .T. ) ;
#205532=FACE_BOUND ( 'NONE', #48557, .T. ) ;
#205584=CARTESIAN_POINT ( 'NONE',  ( 23.24999999999999645, 8.822561741677553471, -76.25000000000004263 ) ) ;
#205674=LINE ( 'NONE', #109141, #76714 ) ;
#205687=ORIENTED_EDGE ( 'NONE', *, *, #208451, .T. ) ;
#205820=CARTESIAN_POINT ( 'NONE',  ( -18.40000000000000213, 11.48667500176882861, -91.25000000000005684 ) ) ;
#205922=ORIENTED_EDGE ( 'NONE', *, *, #47963, .T. ) ;
#205942=B_SPLINE_CURVE_WITH_KNOTS ( 'NONE', 3,
 ( #179054, #117754, #120366, #239000, #19962, #159461, #42100, #221962, #121637, #257217, #198571, #201144, #102015, #219408 ),
 .UNSPECIFIED., .F., .F.,
 ( 4, 2, 2, 2, 2, 2, 4 ),
 ( 0.000000000000000000, 2.389617747645615524E-05, 4.779235495291231047E-05, 9.558470990578232351E-05, 0.0001911694198114826000, 0.0003823388396228848064, 0.0007646776792456892735 ),
 .UNSPECIFIED. ) ;
#206025=VERTEX_POINT ( 'NONE', #167105 ) ;
#206131=CARTESIAN_POINT ( 'NONE',  ( -16.93826681692523550, 10.01142872029886810, -87.94545846735948658 ) ) ;
#206287=( BOUNDED_CURVE ( )  B_SPLINE_CURVE ( 3, ( #4907, #140586, #222680, #123608 ),
 .UNSPECIFIED., .F., .F. ) 
 B_SPLINE_CURVE_WITH_KNOTS ( ( 4, 4 ),
 ( 5.731445031868799056, 5.983100554402348337 ),
 .UNSPECIFIED. ) 
 CURVE ( )  GEOMETRIC_REPRESENTATION_ITEM ( )  RATIONAL_B_SPLINE_CURVE ( ( 1.000000000000000000, 0.9947294176030464508, 0.9947294176030464508, 1.000000000000000000 ) ) 
 REPRESENTATION_ITEM ( '' )  );
#206327=ORIENTED_EDGE ( 'NONE', *, *, #11332, .T. ) ;
#206484=VECTOR ( 'NONE', #110065, 1000.000000000000000 ) ;
#206507=EDGE_CURVE ( 'NONE', #103997, #67043, #87204, .T. ) ;
#206519=CARTESIAN_POINT ( 'NONE',  ( -16.80621392010910498, 9.942202577518919782, -87.81040803458310506 ) ) ;
#206576=VECTOR ( 'NONE', #254903, 1000.000000000000000 ) ;
#206702=DIRECTION ( 'NONE',  ( 1.000000000000000000, -0.000000000000000000, -0.000000000000000000 ) ) ;
#206794=EDGE_CURVE ( 'NONE', #45686, #65351, #73486, .T. ) ;
#206885=PLANE ( 'NONE',  #178435 ) ;
#206898=CARTESIAN_POINT ( 'NONE',  ( -13.54036565897074773, 9.451541661396667848, -85.45387549883064082 ) ) ;
#206925=EDGE_CURVE ( 'NONE', #236242, #152148, #68009, .T. ) ;
#206969=EDGE_CURVE ( 'NONE', #214712, #41600, #43323, .T. ) ;
#207087=ORIENTED_EDGE ( 'NONE', *, *, #161626, .T. ) ;
#207166=CARTESIAN_POINT ( 'NONE',  ( -20.65000000000000568, 5.650000000011139001, -76.25000000000004263 ) ) ;
#207289=EDGE_CURVE ( 'NONE', #65351, #39843, #144660, .T. ) ;
#207867=DIRECTION ( 'NONE',  ( 1.000000000000000000, 0.000000000000000000, -1.020425574104004196E-15 ) ) ;
#207901=CARTESIAN_POINT ( 'NONE',  ( -17.11825945287482753, 9.950000000011140600, -79.65000000000006253 ) ) ;
#207925=VERTEX_POINT ( 'NONE', #114220 ) ;
#207933=ORIENTED_EDGE ( 'NONE', *, *, #215047, .F. ) ;
#208029=CARTESIAN_POINT ( 'NONE',  ( -16.89021194854740315, 9.950000000011137047, -87.74256813160438639 ) ) ;
#208356=DIRECTION ( 'NONE',  ( 0.000000000000000000, -0.000000000000000000, -1.000000000000000000 ) ) ;
#208399=ORIENTED_EDGE ( 'NONE', *, *, #117763, .T. ) ;
#208451=EDGE_CURVE ( 'NONE', #13912, #56045, #22395, .T. ) ;
#208720=CARTESIAN_POINT ( 'NONE',  ( -21.64999999999999858, 10.05000000001113847, -87.75000000000005684 ) ) ;
#208780=DIRECTION ( 'NONE',  ( -1.000000000000000000, 0.000000000000000000, 0.000000000000000000 ) ) ;
#209016=VECTOR ( 'NONE', #85300, 1000.000000000000000 ) ;
#209164=ORIENTED_EDGE ( 'NONE', *, *, #227514, .T. ) ;
#209299=CARTESIAN_POINT ( 'NONE',  ( -18.41431012584569160, 11.48747202921932242, -76.22676398689837640 ) ) ;
#209459=CARTESIAN_POINT ( 'NONE',  ( -15.73854595235692244, 9.351413679112546617, -83.98034356754902774 ) ) ;
#209865=ORIENTED_EDGE ( 'NONE', *, *, #31425, .T. ) ;
#210248=LINE ( 'NONE', #51128, #189284 ) ;
#210266=CARTESIAN_POINT ( 'NONE',  ( -16.89268316805465986, 9.951721813253337601, -87.85575247854558256 ) ) ;
#210454=DIRECTION ( 'NONE',  ( 0.7071067811865493491, 0.7071067811865456854, 0.000000000000000000 ) ) ;
#210580=CARTESIAN_POINT ( 'NONE',  ( -16.90138253750127006, 9.950000000011137047, -87.71156270790466181 ) ) ;
#210770=DIRECTION ( 'NONE',  ( -0.7071067811865463515, -0.7071067811865487940, 7.587431340288849180E-16 ) ) ;
#210817=AXIS2_PLACEMENT_3D ( 'NONE', #193856, #12668, #210846 ) ;
#210835=ORIENTED_EDGE ( 'NONE', *, *, #3112, .T. ) ;
#210846=DIRECTION ( 'NONE',  ( -1.020425574104004196E-15, -1.210927747993693964E-31, 1.000000000000000000 ) ) ;
#210996=AXIS2_PLACEMENT_3D ( 'NONE', #183025, #203847, #25237 ) ;
#211163=ORIENTED_EDGE ( 'NONE', *, *, #107470, .F. ) ;
#211378=VECTOR ( 'NONE', #142406, 1000.000000000000000 ) ;
#211504=ORIENTED_EDGE ( 'NONE', *, *, #257033, .F. ) ;
#211513=CYLINDRICAL_SURFACE ( 'NONE', #54996, 0.1999999999999987899 ) ;
#211534=EDGE_CURVE ( 'NONE', #77128, #129272, #217370, .T. ) ;
#211580=LINE ( 'NONE', #112486, #130899 ) ;
#211739=PLANE ( 'NONE',  #248953 ) ;
#211776=ORIENTED_EDGE ( 'NONE', *, *, #30682, .F. ) ;
#211880=CARTESIAN_POINT ( 'NONE',  ( -16.97683809663755028, 9.950000000011142376, -87.22847083211067343 ) ) ;
#211917=CARTESIAN_POINT ( 'NONE',  ( -13.77178122865953824, 9.456028260519072859, -82.01119803506577455 ) ) ;
#212231=DIRECTION ( 'NONE',  ( -0.000000000000000000, 0.000000000000000000, -1.000000000000000000 ) ) ;
#212464=EDGE_CURVE ( 'NONE', #14621, #198491, #237455, .T. ) ;
#213027=CARTESIAN_POINT ( 'NONE',  ( -16.94445028196808778, 9.992063609708889516, -79.60733017841850767 ) ) ;
#213247=CARTESIAN_POINT ( 'NONE',  ( -15.75000000000000355, 9.850000000011133849, -83.75000000000004263 ) ) ;
#213324=CARTESIAN_POINT ( 'NONE',  ( -16.90257928357874562, 9.954106821116520010, -79.63628543011373040 ) ) ;
#213418=( NAMED_UNIT ( * ) SI_UNIT ( $, .STERADIAN. ) SOLID_ANGLE_UNIT ( ) );
#213439=EDGE_LOOP ( 'NONE', ( #101053, #26332, #237447, #205369 ) ) ;
#213488=CARTESIAN_POINT ( 'NONE',  ( -16.87368910959167678, 9.961273816702552963, -79.61249309664063389 ) ) ;
#213496=VECTOR ( 'NONE', #185884, 1000.000000000000000 ) ;
#214034=DIRECTION ( 'NONE',  ( 1.000000000000000000, -0.000000000000000000, -0.000000000000000000 ) ) ;
#214108=LINE ( 'NONE', #111153, #144442 ) ;
#214266=CARTESIAN_POINT ( 'NONE',  ( -16.87683809663752754, 9.865889849343227880, -80.26742680707030786 ) ) ;
#214458=EDGE_LOOP ( 'NONE', ( #166992, #115879, #21210, #55236 ) ) ;
#214480=EDGE_CURVE ( 'NONE', #102037, #146336, #167245, .T. ) ;
#214554=CARTESIAN_POINT ( 'NONE',  ( -16.78569801330232636, 9.947933733124651567, -79.65691290534755353 ) ) ;
#214712=VERTEX_POINT ( 'NONE', #238739 ) ;
#215047=EDGE_CURVE ( 'NONE', #158005, #128159, #7983, .T. ) ;
#215134=CARTESIAN_POINT ( 'NONE',  ( 15.69410316191958898, 9.356746017089403011, -84.20335972136422242 ) ) ;
#215165=EDGE_CURVE ( 'NONE', #128159, #158005, #153771, .T. ) ;
#215174=CARTESIAN_POINT ( 'NONE',  ( -18.40000000000000213, 11.75000000001113953, -87.85000000000003695 ) ) ;
#215223=CARTESIAN_POINT ( 'NONE',  ( -18.35668295345803713, 11.47316190337363118, -91.25000000000005684 ) ) ;
#215538=CARTESIAN_POINT ( 'NONE',  ( -16.87401514999241314, 9.950000000011137047, -79.71998200746823215 ) ) ;
#215691=LINE ( 'NONE', #177887, #165722 ) ;
#215752=DIRECTION ( 'NONE',  ( 1.000000000000000000, 0.000000000000000000, -0.000000000000000000 ) ) ;
#215886=CARTESIAN_POINT ( 'NONE',  ( -17.73285935861373019, 10.85798180380192335, -90.25856180978082932 ) ) ;
#215889=CARTESIAN_POINT ( 'NONE',  ( -16.89146115310546037, 9.951443245667611848, -87.85482241895425659 ) ) ;
#215895=DIRECTION ( 'NONE',  ( 1.186688945009010077E-16, -1.000000000000000000, -0.000000000000000000 ) ) ;
#215930=PLANE ( 'NONE',  #173916 ) ;
#216085=DIRECTION ( 'NONE',  ( -1.000000000000000000, 0.000000000000000000, 0.000000000000000000 ) ) ;
#216144=EDGE_LOOP ( 'NONE', ( #197885, #119121, #65556, #167120, #115840, #62704 ) ) ;
#216209=AXIS2_PLACEMENT_3D ( 'NONE', #150240, #96316, #195468 ) ;
#216365=ORIENTED_EDGE ( 'NONE', *, *, #49510, .F. ) ;
#216373=CARTESIAN_POINT ( 'NONE',  ( -17.71734398241073194, 10.84235722847571459, -90.22513825300563894 ) ) ;
#216465=CIRCLE ( 'NONE', #104004, 0.1999999999999987899 ) ;
#216571=ORIENTED_EDGE ( 'NONE', *, *, #160867, .F. ) ;
#216817=CARTESIAN_POINT ( 'NONE',  ( -16.77180007708460963, 9.950000000011137047, -79.63561411895486231 ) ) ;
#217065=VECTOR ( 'NONE', #66636, 1000.000000000000000 ) ;
#217173=CARTESIAN_POINT ( 'NONE',  ( -17.78241384941129155, 10.85557575279901066, -90.25096232753028858 ) ) ;
#217323=CARTESIAN_POINT ( 'NONE',  ( -16.89268316805466341, 9.951721813253341153, -79.64424752145448849 ) ) ;
#217340=EDGE_LOOP ( 'NONE', ( #179386, #102185, #79617, #60274, #84563 ) ) ;
#217370=LINE ( 'NONE', #59560, #123225 ) ;
#217430=VECTOR ( 'NONE', #44607, 1000.000000000000000 ) ;
#217557=LINE ( 'NONE', #20682, #30789 ) ;
#217602=ORIENTED_EDGE ( 'NONE', *, *, #183258, .F. ) ;
#217780=CARTESIAN_POINT ( 'NONE',  ( -12.25000000000000178, 9.350000000011139178, -83.75000000000004263 ) ) ;
#218042=VERTEX_POINT ( 'NONE', #29077 ) ;
#218264=DIRECTION ( 'NONE',  ( 0.7071067811865456854, -0.7071067811865493491, -0.000000000000000000 ) ) ;
#218342=DIRECTION ( 'NONE',  ( -3.035766082959430717E-14, 0.000000000000000000, -1.000000000000000000 ) ) ;
#218746=PRESENTATION_STYLE_ASSIGNMENT (( #26686 ) ) ;
#218936=CARTESIAN_POINT ( 'NONE',  ( 15.74999999999999645, 9.350000000011139178, -83.75000000000004263 ) ) ;
#219172=CARTESIAN_POINT ( 'NONE',  ( 16.87683809663750267, 9.950000000011138823, -79.65000000000003411 ) ) ;
#219258=DIRECTION ( 'NONE',  ( -1.000000000000000000, -0.000000000000000000, 1.073024830501117725E-15 ) ) ;
#219355=CARTESIAN_POINT ( 'NONE',  ( -16.83794479845801817, 9.926357419362647150, -87.69644470422234406 ) ) ;
#219394=VECTOR ( 'NONE', #107376, 1000.000000000000000 ) ;
#219408=CARTESIAN_POINT ( 'NONE',  ( -16.87683809663752399, 9.850000000011144508, -80.40236401819635148 ) ) ;
#219488=CARTESIAN_POINT ( 'NONE',  ( -16.90137573187933739, 9.950000000011135270, -79.78841742409694859 ) ) ;
#219649=DIRECTION ( 'NONE',  ( 0.000000000000000000, 1.000000000000000000, -0.000000000000000000 ) ) ;
#219656=AXIS2_PLACEMENT_3D ( 'NONE', #118442, #197952, #19327 ) ;
#219674=VERTEX_POINT ( 'NONE', #29806 ) ;
#219681=ORIENTED_EDGE ( 'NONE', *, *, #91337, .T. ) ;
#220018=VECTOR ( 'NONE', #5247, 1000.000000000000000 ) ;
#220106=ORIENTED_EDGE ( 'NONE', *, *, #256211, .T. ) ;
#220211=CARTESIAN_POINT ( 'NONE',  ( -16.81744102076748959, 9.950000000011138823, -87.85000000000005116 ) ) ;
#220213=DIRECTION ( 'NONE',  ( -0.000000000000000000, 1.000000000000000000, -0.000000000000000000 ) ) ;
#220249=CARTESIAN_POINT ( 'NONE',  ( 12.84233041328156055, 9.410538608540026217, -82.43268799714094541 ) ) ;
#220342=AXIS2_PLACEMENT_3D ( 'NONE', #208720, #169623, #186585 ) ;
#220509=AXIS2_PLACEMENT_3D ( 'NONE', #252975, #118632, #96453 ) ;
#220662=AXIS2_PLACEMENT_3D ( 'NONE', #71256, #92071, #171655 ) ;
#220779=DIRECTION ( 'NONE',  ( -1.000000000000000000, 0.000000000000000000, 0.000000000000000000 ) ) ;
#220890=CARTESIAN_POINT ( 'NONE',  ( -15.75000000000000355, 9.350000000011140955, -83.75000000000004263 ) ) ;
#220922=CARTESIAN_POINT ( 'NONE',  ( -16.88783316861814399, 9.950000000011137047, -87.74773595802028581 ) ) ;
#220970=CARTESIAN_POINT ( 'NONE',  ( -16.77683809663752257, 9.945835743215301505, -79.66394901910425119 ) ) ;
#220984=VECTOR ( 'NONE', #239463, 1000.000000000000000 ) ;
#221258=DIRECTION ( 'NONE',  ( 1.000000000000000000, 0.000000000000000000, 0.000000000000000000 ) ) ;
#221312=CARTESIAN_POINT ( 'NONE',  ( -18.40000000000000213, 11.41458325961095177, -87.85000000000003695 ) ) ;
#221487=FACE_OUTER_BOUND ( 'NONE', #9615, .T. ) ;
#221510=CARTESIAN_POINT ( 'NONE',  ( -20.65000000000000568, 5.650000000011139001, -87.85000000000003695 ) ) ;
#221677=AXIS2_PLACEMENT_3D ( 'NONE', #121163, #200669, #159001 ) ;
#221811=EDGE_CURVE ( 'NONE', #176792, #248456, #100364, .T. ) ;
#221903=CARTESIAN_POINT ( 'NONE',  ( -16.77683809663752257, 9.945835743215303282, -87.83605098089584828 ) ) ;
#221962=CARTESIAN_POINT ( 'NONE',  ( -16.83199030136658081, 9.930648033124620966, -79.77240102265751887 ) ) ;
#222036=CARTESIAN_POINT ( 'NONE',  ( -16.86132326855785735, 9.950000000011135270, -79.69863578466836884 ) ) ;
#222198=CARTESIAN_POINT ( 'NONE',  ( -16.82055514392389028, 9.950000000011137047, -87.82320192545805071 ) ) ;
#222422=ADVANCED_FACE ( 'NONE', ( #243438 ), #206885, .F. ) ;
#222474=CARTESIAN_POINT ( 'NONE',  ( -21.65000000000000213, 7.250000000011138646, -87.85000000000003695 ) ) ;
#222532=CARTESIAN_POINT ( 'NONE',  ( -18.40000000000000213, 11.75000000001113953, -91.25000000000005684 ) ) ;
#222612=ORIENTED_EDGE ( 'NONE', *, *, #107470, .T. ) ;
#222680=CARTESIAN_POINT ( 'NONE',  ( -17.22361732159832215, 10.34515565861359221, -78.37078452586717958 ) ) ;
#222707=VERTEX_POINT ( 'NONE', #20252 ) ;
#222960=ADVANCED_FACE ( 'NONE', ( #52636 ), #211739, .F. ) ;
#223162=CARTESIAN_POINT ( 'NONE',  ( -18.40000000000000213, 11.33174054713631662, -79.65000000000004832 ) ) ;
#223305=VECTOR ( 'NONE', #249133, 1000.000000000000000 ) ;
#223588=ORIENTED_EDGE ( 'NONE', *, *, #207289, .F. ) ;
#223604=VECTOR ( 'NONE', #23598, 1000.000000000000000 ) ;
#223850=TOROIDAL_SURFACE ( 'NONE', #44808, 14.20833333333334103, 0.1000000000000000056 ) ;
#223869=DIRECTION ( 'NONE',  ( 0.000000000000000000, 0.000000000000000000, 1.000000000000000000 ) ) ;
#223962=DIRECTION ( 'NONE',  ( -0.000000000000000000, 1.000000000000000000, -0.000000000000000000 ) ) ;
#223995=B_SPLINE_CURVE_WITH_KNOTS ( 'NONE', 3,
 ( #181543, #114157, #2866, #160712, #60279, #219355, #75069, #306, #159408, #122848, #82388, #161987, #241500, #221903 ),
 .UNSPECIFIED., .F., .F.,
 ( 4, 2, 2, 2, 2, 2, 4 ),
 ( 1.398578778534940505E-17, 0.0003823333598417389258, 0.0005735000397626219141, 0.0006690833797230837099, 0.0007168750497033132526, 0.0007407708846934279697, 0.0007646667196835427952 ),
 .UNSPECIFIED. ) ;
#224032=CARTESIAN_POINT ( 'NONE',  ( 20.04999999999999716, 8.750000000011173285, -87.85000000000003695 ) ) ;
#224067=CARTESIAN_POINT ( 'NONE',  ( 14.11444803880196552, 9.457431528860066550, -81.99991693789971237 ) ) ;
#224439=AXIS2_PLACEMENT_3D ( 'NONE', #81884, #101434, #139306 ) ;
#224633=ORIENTED_EDGE ( 'NONE', *, *, #150054, .T. ) ;
#224750=CARTESIAN_POINT ( 'NONE',  ( 18.39999999999999503, 11.47316190337363828, -91.25000000000005684 ) ) ;
#224756=DIRECTION ( 'NONE',  ( -0.000000000000000000, 1.000000000000000000, -0.000000000000000000 ) ) ;
#224778=CARTESIAN_POINT ( 'NONE',  ( -16.92280123533709357, 9.950000000011137047, -87.64936768591496730 ) ) ;
#224851=FILL_AREA_STYLE ('',( #205282 ) ) ;
#224908=VECTOR ( 'NONE', #60766, 1000.000000000000000 ) ;
#225061=CARTESIAN_POINT ( 'NONE',  ( -16.92778301347296122, 10.00094491684659381, -87.92851810796820189 ) ) ;
#225818=LINE ( 'NONE', #47187, #161331 ) ;
#226004=ADVANCED_FACE ( 'NONE', ( #27166 ), #167955, .F. ) ;
#226324=LINE ( 'NONE', #222474, #134308 ) ;
#226348=ORIENTED_EDGE ( 'NONE', *, *, #50756, .T. ) ;
#226551=ADVANCED_FACE ( 'NONE', ( #30700 ), #92739, .T. ) ;
#226710=B_SPLINE_CURVE_WITH_KNOTS ( 'NONE', 3,
 ( #256403, #94824, #16603, #97360, #156122, #192660, #213488, #77819, #157414, #217323 ),
 .UNSPECIFIED., .F., .F.,
 ( 4, 3, 3, 4 ),
 ( 0.000000000000000000, 4.874959354401679605E-05, 9.785140065120178569E-05, 0.0001360444631935948218 ),
 .UNSPECIFIED. ) ;
#226975=CARTESIAN_POINT ( 'NONE',  ( -16.94132844910801694, 9.992436755191498321, -87.89620175598236074 ) ) ;
#227220=DIRECTION ( 'NONE',  ( -0.000000000000000000, 1.000000000000000000, -0.000000000000000000 ) ) ;
#227393=DIRECTION ( 'NONE',  ( -1.000000000000000000, 0.000000000000000000, 0.000000000000000000 ) ) ;
#227514=EDGE_CURVE ( 'NONE', #8126, #143848, #11321, .T. ) ;
#227517=CARTESIAN_POINT ( 'NONE',  ( 18.39999999999999503, 5.650000000011139001, -91.25000000000005684 ) ) ;
#227635=( BOUNDED_SURFACE ( )  B_SPLINE_SURFACE ( 3, 2, ( 
 ( #149207, #207901, #68370 ),
 ( #171367, #147914, #89200 ),
 ( #87895, #29285, #110052 ),
 ( #245720, #250836, #9670 ) ),
 .UNSPECIFIED., .F., .F., .F. ) 
 B_SPLINE_SURFACE_WITH_KNOTS ( ( 4, 4 ),
 ( 3, 3 ),
 ( 4.712388980384689674, 5.765869716888459173 ),
 ( 0.000000000000000000, 1.000000000000000000 ),
 .UNSPECIFIED. ) 
 GEOMETRIC_REPRESENTATION_ITEM ( )  RATIONAL_B_SPLINE_SURFACE ( (
 ( 1.000000000000000000, 0.7071067811865475727, 1.000000000000000000),
 ( 1.000000000000000000, 0.7953136715913110555, 1.000000000000000000),
 ( 1.000000000000000000, 0.8646876308615464302, 1.000000000000000000),
 ( 1.000000000000000000, 0.8984936768950617658, 1.000000000000000000) ) ) 
 REPRESENTATION_ITEM ( '' )  SURFACE ( )  );
#227720=UNCERTAINTY_MEASURE_WITH_UNIT (LENGTH_MEASURE( 1.000000000000000082E-05 ), #7090, 'distance_accuracy_value', 'NONE');
#227770=CARTESIAN_POINT ( 'NONE',  ( -16.87331047859649757, 9.950000000011138823, -87.85000000000005116 ) ) ;
#227878=DIRECTION ( 'NONE',  ( 0.000000000000000000, 1.000000000000000000, 0.000000000000000000 ) ) ;
#228190=CARTESIAN_POINT ( 'NONE',  ( 18.39999999999999503, 11.75000000001113953, -79.65000000000004832 ) ) ;
#228270=CARTESIAN_POINT ( 'NONE',  ( -16.93658211146644987, 9.994108662352344297, -87.90429506995572240 ) ) ;
#228325=AXIS2_PLACEMENT_3D ( 'NONE', #101930, #21174, #64121 ) ;
#228775=VERTEX_POINT ( 'NONE', #244515 ) ;
#228882=CARTESIAN_POINT ( 'NONE',  ( -18.34374000495060386, 11.47316190337362585, -76.25000000000004263 ) ) ;
#228901=CARTESIAN_POINT ( 'NONE',  ( -12.25000000000000000, 9.350000000011133849, -83.51856895740269238 ) ) ;
#229007=VERTEX_POINT ( 'NONE', #14921 ) ;
#229063=AXIS2_PLACEMENT_3D ( 'NONE', #157466, #32384, #96148 ) ;
#229338=ORIENTED_EDGE ( 'NONE', *, *, #152927, .F. ) ;
#229466=CARTESIAN_POINT ( 'NONE',  ( 20.73486653747088937, 7.750000000011182166, -87.85000000000003695 ) ) ;
#229709=ORIENTED_EDGE ( 'NONE', *, *, #121254, .T. ) ;
#229980=LINE ( 'NONE', #31817, #209016 ) ;
#230028=CARTESIAN_POINT ( 'NONE',  ( -16.93302609847409457, 9.996682520814371031, -79.58638849536259841 ) ) ;
#230152=CARTESIAN_POINT ( 'NONE',  ( -17.73285935861319373, 10.85798180380184341, -77.24143819021939805 ) ) ;
#230278=EDGE_CURVE ( 'NONE', #45686, #242585, #215691, .T. ) ;
#230390=LINE ( 'NONE', #51721, #102420 ) ;
#230407=EDGE_CURVE ( 'NONE', #32954, #229007, #147590, .T. ) ;
#230577=ORIENTED_EDGE ( 'NONE', *, *, #113535, .F. ) ;
#230867=CARTESIAN_POINT ( 'NONE',  ( 15.57250062127604373, 9.370689921613767126, -84.52646512666112244 ) ) ;
#230922=ADVANCED_FACE ( 'NONE', ( #238768 ), #135794, .T. ) ;
#231094=EDGE_LOOP ( 'NONE', ( #177673, #115205, #197366, #6685 ) ) ;
#231333=CARTESIAN_POINT ( 'NONE',  ( -16.93906926870270624, 10.01214687095770906, -79.55345230722686267 ) ) ;
#231376=CARTESIAN_POINT ( 'NONE',  ( -16.97683809663752896, 9.950000000011140600, -80.27152476867001951 ) ) ;
#231479=CARTESIAN_POINT ( 'NONE',  ( -13.54795643572457919, 9.450668889178682974, -82.05554649020740499 ) ) ;
#231487=AXIS2_PLACEMENT_3D ( 'NONE', #113111, #251322, #212231 ) ;
#231497=LINE ( 'NONE', #52828, #49398 ) ;
#231599=PLANE ( 'NONE',  #68408 ) ;
#231607=CARTESIAN_POINT ( 'NONE',  ( -12.30589683808040213, 9.356746017089404788, -84.20335972136423663 ) ) ;
#231611=LINE ( 'NONE', #15128, #114187 ) ;
#231889=ORIENTED_EDGE ( 'NONE', *, *, #206969, .T. ) ;
#232145=CARTESIAN_POINT ( 'NONE',  ( 12.25000000000000178, 9.350000000011140955, -83.86426760761612798 ) ) ;
#232265=ADVANCED_FACE ( 'NONE', ( #203535 ), #24918, .F. ) ;
#232365=EDGE_LOOP ( 'NONE', ( #22148, #163851, #90462, #156539, #67286 ) ) ;
#232463=CARTESIAN_POINT ( 'NONE',  ( 18.39999999999999503, 11.75000000001113953, -87.85000000000003695 ) ) ;
#232741=CARTESIAN_POINT ( 'NONE',  ( -17.78241384942103309, 10.85557575279231735, -77.24903767246566133 ) ) ;
#232805=VERTEX_POINT ( 'NONE', #47667 ) ;
#232844=DIRECTION ( 'NONE',  ( 1.186688945009010077E-16, -1.000000000000000000, -0.000000000000000000 ) ) ;
#233341=VERTEX_POINT ( 'NONE', #10831 ) ;
#233395=FACE_OUTER_BOUND ( 'NONE', #11580, .T. ) ;
#233488=CIRCLE ( 'NONE', #96068, 1.749999999999999778 ) ;
#234010=ADVANCED_FACE ( 'NONE', ( #165117 ), #12812, .T. ) ;
#234039=ORIENTED_EDGE ( 'NONE', *, *, #160744, .F. ) ;
#234118=CARTESIAN_POINT ( 'NONE',  ( -16.80438519320023616, 9.949779096479501206, -79.65073828092131691 ) ) ;
#234143=DIRECTION ( 'NONE',  ( -1.000000000000000000, -1.646408749285562691E-14, 0.000000000000000000 ) ) ;
#234700=CARTESIAN_POINT ( 'NONE',  ( 13.77030915526558630, 9.456007326080463571, -85.48863349414679647 ) ) ;
#234910=CARTESIAN_POINT ( 'NONE',  ( 17.23472005113827876, 10.30788195451192379, -78.45342313993134553 ) ) ;
#235090=EDGE_CURVE ( 'NONE', #181633, #102764, #229980, .T. ) ;
#235117=CARTESIAN_POINT ( 'NONE',  ( -16.88783316861809780, 9.950000000011137047, -79.75226404197984209 ) ) ;
#235462=CARTESIAN_POINT ( 'NONE',  ( -17.29838795459022194, 10.37154985796385276, -89.10474128261724047 ) ) ;
#235704=CARTESIAN_POINT ( 'NONE',  ( -20.65000000000000568, 7.250000000011138646, -87.85000000000003695 ) ) ;
#235757=CARTESIAN_POINT ( 'NONE',  ( 20.99999999999999645, 9.750000000011137757, -76.25000000000004263 ) ) ;
#235844=PLANE ( 'NONE',  #130597 ) ;
#236168=VERTEX_POINT ( 'NONE', #45279 ) ;
#236242=VERTEX_POINT ( 'NONE', #51665 ) ;
#236388=CARTESIAN_POINT ( 'NONE',  ( -16.79270642812321412, 9.946244216949081007, -79.66106672143797596 ) ) ;
#236480=CARTESIAN_POINT ( 'NONE',  ( 20.27550659511088682, 9.216043722520002035, -79.65000000000004832 ) ) ;
#236546=CARTESIAN_POINT ( 'NONE',  ( -18.40000000000000213, 11.75000000001113953, -87.85000000000003695 ) ) ;
#236548=LINE ( 'NONE', #179186, #186037 ) ;
#236703=CARTESIAN_POINT ( 'NONE',  ( -18.34804628011471195, 11.47316190337353525, -76.25000000000004263 ) ) ;
#236745=CARTESIAN_POINT ( 'NONE',  ( -16.88853107394619357, 9.950878483358135185, -87.85293634689227815 ) ) ;
#236835=FILL_AREA_STYLE ('',( #195184 ) ) ;
#237225=DIRECTION ( 'NONE',  ( -1.000000000000000000, 0.000000000000000000, 0.000000000000000000 ) ) ;
#237233=CARTESIAN_POINT ( 'NONE',  ( 12.25000000000000000, 9.350000000011140955, -83.75000000000004263 ) ) ;
#237234=CIRCLE ( 'NONE', #220662, 0.1999999999999987899 ) ;
#237447=ORIENTED_EDGE ( 'NONE', *, *, #250046, .T. ) ;
#237455=( BOUNDED_CURVE ( )  B_SPLINE_CURVE ( 3, ( #124811, #141787, #221312, #101332 ),
 .UNSPECIFIED., .F., .F. ) 
 B_SPLINE_CURVE_WITH_KNOTS ( ( 4, 4 ),
 ( 0.000000000000000000, 1.570796326794896558 ),
 .UNSPECIFIED. ) 
 CURVE ( )  GEOMETRIC_REPRESENTATION_ITEM ( )  RATIONAL_B_SPLINE_CURVE ( ( 1.000000000000000000, 0.8047378541243649375, 0.8047378541243649375, 1.000000000000000000 ) ) 
 REPRESENTATION_ITEM ( '' )  );
#237556=CARTESIAN_POINT ( 'NONE',  ( 20.05000000000002913, 7.250000000011171508, -79.65000000000004832 ) ) ;
#237679=CARTESIAN_POINT ( 'NONE',  ( -16.82542659449987354, 9.934499891438514751, -79.74463560002654106 ) ) ;
#238036=EDGE_CURVE ( 'NONE', #146041, #170888, #10998, .T. ) ;
#238093=EDGE_CURVE ( 'NONE', #103997, #181633, #160861, .T. ) ;
#238322=SURFACE_SIDE_STYLE ('',( #158821 ) ) ;
#238379=CARTESIAN_POINT ( 'NONE',  ( -21.64999999999999858, 10.05000000001113847, -79.65000000000004832 ) ) ;
#238415=FACE_OUTER_BOUND ( 'NONE', #231094, .T. ) ;
#238688=CARTESIAN_POINT ( 'NONE',  ( -16.87036670365548474, 10.08494996326643189, -87.95000000000004547 ) ) ;
#238739=CARTESIAN_POINT ( 'NONE',  ( -18.40000000000000213, 11.48667500176882328, -76.25000000000004263 ) ) ;
#238768=FACE_OUTER_BOUND ( 'NONE', #189478, .T. ) ;
#238849=DIRECTION ( 'NONE',  ( -0.000000000000000000, -0.000000000000000000, -1.000000000000000000 ) ) ;
#238971=CARTESIAN_POINT ( 'NONE',  ( -16.87998658237754768, 9.950000000011137047, -79.86363956773804773 ) ) ;
#239000=CARTESIAN_POINT ( 'NONE',  ( -16.80100426158790583, 9.943150520407293413, -79.68294575283408676 ) ) ;
#239059=DIRECTION ( 'NONE',  ( 0.5932847527679310229, -0.8049926720990042694, -6.366092712777067056E-16 ) ) ;
#239130=DIRECTION ( 'NONE',  ( -0.000000000000000000, -0.000000000000000000, -1.000000000000000000 ) ) ;
#239287=CARTESIAN_POINT ( 'NONE',  ( -16.87036670365548474, 9.989418819312801290, -87.97956011730209980 ) ) ;
#239463=DIRECTION ( 'NONE',  ( 1.020425574104004196E-15, 1.210927747993693964E-31, 1.000000000000000000 ) ) ;
#239486=DIRECTION ( 'NONE',  ( -0.000000000000000000, 1.000000000000000000, -0.000000000000000000 ) ) ;
#239840=ORIENTED_EDGE ( 'NONE', *, *, #180711, .T. ) ;
#239944=B_SPLINE_CURVE_WITH_KNOTS ( 'NONE', 3,
 ( #149786, #91072, #92346, #109328 ),
 .UNSPECIFIED., .F., .F.,
 ( 4, 4 ),
 ( 0.000000000000000000, 7.713889350927600000E-05 ),
 .UNSPECIFIED. ) ;
#239978=FACE_OUTER_BOUND ( 'NONE', #17300, .T. ) ;
#240050=ORIENTED_EDGE ( 'NONE', *, *, #14549, .F. ) ;
#240127=LINE ( 'NONE', #124034, #186706 ) ;
#240504=CARTESIAN_POINT ( 'NONE',  ( -16.87333278164152972, 9.882609784590000501, -87.36683219384656240 ) ) ;
#240576=DIRECTION ( 'NONE',  ( 0.2834754621636439431, -0.2834754621636535465, -0.9161240771326838450 ) ) ;
#240850=DIRECTION ( 'NONE',  ( 0.000000000000000000, 0.000000000000000000, -1.000000000000000000 ) ) ;
#240889=CARTESIAN_POINT ( 'NONE',  ( -17.04761207306817639, 10.02645087340892438, -87.85000000000002274 ) ) ;
#240996=CARTESIAN_POINT ( 'NONE',  ( -16.87331047859649757, 9.950000000011138823, -87.85000000000005116 ) ) ;
#241036=DIRECTION ( 'NONE',  ( 1.000000000000000000, 0.000000000000000000, 0.000000000000000000 ) ) ;
#241236=DIRECTION ( 'NONE',  ( -1.000000000000000000, 0.000000000000000000, 0.000000000000000000 ) ) ;
#241278=DIRECTION ( 'NONE',  ( 0.2834754621636358940, -0.2834754621636437211, 0.9161240771326893961 ) ) ;
#241355=VERTEX_POINT ( 'NONE', #23508 ) ;
#241500=CARTESIAN_POINT ( 'NONE',  ( -16.78493211734303969, 9.945835743215329927, -87.83605098089604724 ) ) ;
#241566=VERTEX_POINT ( 'NONE', #165104 ) ;
#241791=DIRECTION ( 'NONE',  ( -1.000000000000000000, 0.000000000000000000, 0.000000000000000000 ) ) ;
#241881=CARTESIAN_POINT ( 'NONE',  ( -18.40000000000000213, 11.75000000001113953, -91.25000000000005684 ) ) ;
#241976=CARTESIAN_POINT ( 'NONE',  ( -18.34374000495059676, 11.47316190337362940, -91.25000000000005684 ) ) ;
#242229=ORIENTED_EDGE ( 'NONE', *, *, #43022, .F. ) ;
#242328=EDGE_CURVE ( 'NONE', #206025, #177843, #49693, .T. ) ;
#242351=ORIENTED_EDGE ( 'NONE', *, *, #183439, .T. ) ;
#242394=CARTESIAN_POINT ( 'NONE',  ( 13.99999999999999822, 9.850000000011137402, -83.75000000000004263 ) ) ;
#242439=CARTESIAN_POINT ( 'NONE',  ( -18.40000000000000213, 11.47316190337364183, -91.17405393319209850 ) ) ;
#242571=VECTOR ( 'NONE', #147550, 1000.000000000000000 ) ;
#242585=VERTEX_POINT ( 'NONE', #106780 ) ;
#242657=CARTESIAN_POINT ( 'NONE',  ( -16.94445028196807002, 9.992063609708893068, -87.89266982158160602 ) ) ;
#242704=CARTESIAN_POINT ( 'NONE',  ( 22.88900146558018989, 8.703904791123973084, -79.65000000000004832 ) ) ;
#242902=DIRECTION ( 'NONE',  ( -0.000000000000000000, -0.000000000000000000, -1.000000000000000000 ) ) ;
#243433=DIRECTION ( 'NONE',  ( -0.000000000000000000, 1.000000000000000000, -0.000000000000000000 ) ) ;
#243438=FACE_OUTER_BOUND ( 'NONE', #134349, .T. ) ;
#243442=CARTESIAN_POINT ( 'NONE',  ( -16.98495255085916966, 10.00556436600592214, -87.86538279377954552 ) ) ;
#243713=FACE_OUTER_BOUND ( 'NONE', #17790, .T. ) ;
#244159=ORIENTED_EDGE ( 'NONE', *, *, #58847, .T. ) ;
#244240=ORIENTED_EDGE ( 'NONE', *, *, #87893, .F. ) ;
#244247=CARTESIAN_POINT ( 'NONE',  ( -16.94107738177415712, 10.01423928514777728, -79.55000000000005400 ) ) ;
#244256=CARTESIAN_POINT ( 'NONE',  ( -16.78805706634180339, 9.948252493082335945, -87.84415320803191207 ) ) ;
#244347=CARTESIAN_POINT ( 'NONE',  ( -16.80070461187905551, 9.950000000011138823, -87.85303617083869199 ) ) ;
#244515=CARTESIAN_POINT ( 'NONE',  ( -21.65000000000000213, 9.950000000011140600, -79.75000000000004263 ) ) ;
#244560=VECTOR ( 'NONE', #315, 1000.000000000000000 ) ;
#244613=CYLINDRICAL_SURFACE ( 'NONE', #56865, 0.1000000000000001443 ) ;
#244993=LINE ( 'NONE', #63794, #107545 ) ;
#245069=LINE ( 'NONE', #161709, #68695 ) ;
#245720=CARTESIAN_POINT ( 'NONE',  ( -16.87242674293850797, 9.950000000011138823, -79.64890975362770575 ) ) ;
#245723=ORIENTED_EDGE ( 'NONE', *, *, #206507, .T. ) ;
#245805=EDGE_CURVE ( 'NONE', #134549, #78107, #91344, .T. ) ;
#245974=EDGE_CURVE ( 'NONE', #171691, #199040, #195407, .T. ) ;
#246015=UNCERTAINTY_MEASURE_WITH_UNIT (LENGTH_MEASURE( 1.000000000000000082E-05 ), #197710, 'distance_accuracy_value', 'NONE');
#246029=CARTESIAN_POINT ( 'NONE',  ( -13.11924609551134857, 9.431689550535258704, -85.27929003223610493 ) ) ;
#246046=ORIENTED_EDGE ( 'NONE', *, *, #48963, .F. ) ;
#246257=EDGE_CURVE ( 'NONE', #112749, #81779, #204529, .T. ) ;
#246477=ORIENTED_EDGE ( 'NONE', *, *, #204859, .F. ) ;
#246490=CARTESIAN_POINT ( 'NONE',  ( -17.11825945287481687, 10.05000000001113847, -87.85000000000003695 ) ) ;
#246619=( BOUNDED_SURFACE ( )  B_SPLINE_SURFACE ( 3, 2, ( 
 ( #80212, #116814, #39870 ),
 ( #235462, #56801, #21577 ),
 ( #180642, #217173, #215886 ),
 ( #197622, #37295, #178090 ) ),
 .UNSPECIFIED., .F., .F., .F. ) 
 B_SPLINE_SURFACE_WITH_KNOTS ( ( 4, 4 ),
 ( 3, 3 ),
 ( 0.3000847527772381729, 0.5552748953338751958 ),
 ( 0.000000000000000000, 1.000000000000000000 ),
 .UNSPECIFIED. ) 
 GEOMETRIC_REPRESENTATION_ITEM ( )  RATIONAL_B_SPLINE_SURFACE ( (
 ( 1.000000000000000000, 0.9152888060719349683, 1.000000000000000000),
 ( 1.000000000000000000, 0.9104333467450257400, 1.000000000000000000),
 ( 1.000000000000000000, 0.9035312726220622315, 1.000000000000000000),
 ( 1.000000000000000000, 0.8946697475932153809, 1.000000000000000000) ) ) 
 REPRESENTATION_ITEM ( '' )  SURFACE ( )  );
#246954=FACE_OUTER_BOUND ( 'NONE', #53374, .T. ) ;
#247048=ORIENTED_EDGE ( 'NONE', *, *, #58847, .F. ) ;
#247120=CARTESIAN_POINT ( 'NONE',  ( -16.97048361161167307, 9.950000000011138823, -87.35888434443047856 ) ) ;
#247284=CIRCLE ( 'NONE', #176586, 14.20833333333333748 ) ;
#247293=CARTESIAN_POINT ( 'NONE',  ( -14.56336952470180002, 9.446645344706402270, -85.41080645610024646 ) ) ;
#247299=DIRECTION ( 'NONE',  ( -0.000000000000000000, -0.000000000000000000, 1.000000000000000000 ) ) ;
#247352=DIRECTION ( 'NONE',  ( -1.000000000000000000, 0.000000000000000000, 0.000000000000000000 ) ) ;
#247433=CARTESIAN_POINT ( 'NONE',  ( -16.87683809663752399, 23.65833333334447985, -83.75000000000004263 ) ) ;
#247471=EDGE_LOOP ( 'NONE', ( #207933, #242351, #51590, #123684 ) ) ;
#247612=CARTESIAN_POINT ( 'NONE',  ( -16.87331047859651179, 9.950000000011142376, -79.65000000000004832 ) ) ;
#247702=LINE ( 'NONE', #7822, #141492 ) ;
#247822=CARTESIAN_POINT ( 'NONE',  ( -16.93353400591625757, 10.00461239618409515, -87.93268447020545864 ) ) ;
#247958=MECHANICAL_DESIGN_GEOMETRIC_PRESENTATION_REPRESENTATION('',(#60681),#48230);
#248033=ADVANCED_FACE ( 'NONE', ( #126000, #202976, #205532 ), #26942, .T. ) ;
#248152=PLANE ( 'NONE',  #53545 ) ;
#248277=CARTESIAN_POINT ( 'NONE',  ( -16.89797118371649276, 9.976380722655642685, -79.56270663244107766 ) ) ;
#248407=ORIENTED_EDGE ( 'NONE', *, *, #257033, .T. ) ;
#248456=VERTEX_POINT ( 'NONE', #38181 ) ;
#248549=CARTESIAN_POINT ( 'NONE',  ( -16.81744102076749314, 9.950000000011142376, -79.65000000000004832 ) ) ;
#248589=CARTESIAN_POINT ( 'NONE',  ( -15.75000000000000355, 9.350000000011140955, -83.75000000000004263 ) ) ;
#248621=CARTESIAN_POINT ( 'NONE',  ( -16.88005004766534967, 9.950100503332199864, -87.85033611194879200 ) ) ;
#248910=CARTESIAN_POINT ( 'NONE',  ( 23.04999999999999716, 8.822561741677553471, -76.25000000000004263 ) ) ;
#248923=ADVANCED_FACE ( 'NONE', ( #183467 ), #58347, .T. ) ;
#248953=AXIS2_PLACEMENT_3D ( 'NONE', #168796, #210454, #48787 ) ;
#249133=DIRECTION ( 'NONE',  ( 1.652117596168391700E-15, 1.000000000000000000, -0.000000000000000000 ) ) ;
#249498=ORIENTED_EDGE ( 'NONE', *, *, #21597, .T. ) ;
#249535=ORIENTED_EDGE ( 'NONE', *, *, #192, .T. ) ;
#249775=VECTOR ( 'NONE', #208780, 1000.000000000000000 ) ;
#249804=ORIENTED_EDGE ( 'NONE', *, *, #206969, .F. ) ;
#249847=FACE_OUTER_BOUND ( 'NONE', #90495, .T. ) ;
#249874=CARTESIAN_POINT ( 'NONE',  ( -15.31895204843005232, 9.396533993965077158, -84.90593977917338009 ) ) ;
#250046=EDGE_CURVE ( 'NONE', #194746, #171691, #105794, .T. ) ;
#250741=LINE ( 'NONE', #224750, #219394 ) ;
#250836=CARTESIAN_POINT ( 'NONE',  ( -16.91049119928364064, 9.950000000011138823, -79.61827960680922445 ) ) ;
#251001=CARTESIAN_POINT ( 'NONE',  ( -13.12432614554022869, 9.430764995433477793, -82.23053739475051316 ) ) ;
#251017=ADVANCED_FACE ( 'NONE', ( #117728 ), #83288, .F. ) ;
#251051=CARTESIAN_POINT ( 'NONE',  ( -21.65000000000000213, 7.250000000011139534, -79.65000000000004832 ) ) ;
#251135=CARTESIAN_POINT ( 'NONE',  ( -12.25000000000000355, 9.350000000011135626, -83.86574316727397616 ) ) ;
#251322=DIRECTION ( 'NONE',  ( 1.000000000000000000, 0.000000000000000000, -0.000000000000000000 ) ) ;
#251454=DIRECTION ( 'NONE',  ( -1.186688945009010077E-16, 1.000000000000000000, 0.000000000000000000 ) ) ;
#251697=VECTOR ( 'NONE', #187425, 1000.000000000000000 ) ;
#251805=ADVANCED_FACE ( 'NONE', ( #96244 ), #194099, .F. ) ;
#252000=DIRECTION ( 'NONE',  ( 0.000000000000000000, -0.000000000000000000, -1.000000000000000000 ) ) ;
#252290=CARTESIAN_POINT ( 'NONE',  ( -12.93407622233967658, 9.417789466963357725, -82.35738454397692010 ) ) ;
#252413=CARTESIAN_POINT ( 'NONE',  ( -18.34374000495060386, 11.47316190337362585, -76.25000000000004263 ) ) ;
#252492=EDGE_CURVE ( 'NONE', #143362, #48110, #28002, .T. ) ;
#252589=CARTESIAN_POINT ( 'NONE',  ( -16.81744102076749314, 9.950000000011142376, -79.65000000000004832 ) ) ;
#252849=CARTESIAN_POINT ( 'NONE',  ( 13.99999999999999822, 9.850000000011137402, -83.75000000000004263 ) ) ;
#252862=B_SPLINE_CURVE_WITH_KNOTS ( 'NONE', 3,
 ( #237233, #58569, #136834, #138107, #256738, #220249, #160290, #139388, #3750, #199408, #179840, #80700, #102827, #224067, #101531, #119875, #41621, #20769, #122424, #25898, #44177, #83257, #164122, #23349, #121170, #218936 ),
 .UNSPECIFIED., .F., .F.,
 ( 4, 2, 2, 2, 2, 2, 2, 2, 2, 2, 2, 2, 4 ),
 ( 0.005476422646581343041, 0.006160811967703550517, 0.006845201288825757992, 0.007187395949386863464, 0.007529590609947969804, 0.007871785270509074409, 0.008213979931070180748, 0.008556174591631285353, 0.008898369252192391693, 0.009240563912753498033, 0.009582758573314604372, 0.01026714789443681358, 0.01095153721555902800 ),
 .UNSPECIFIED. ) ;
#252888=CIRCLE ( 'NONE', #157241, 0.9000000000000014655 ) ;
#252975=CARTESIAN_POINT ( 'NONE',  ( -14.00000000000000178, 9.850000000011133849, -83.75000000000004263 ) ) ;
#253043=CARTESIAN_POINT ( 'NONE',  ( 23.04999999999999716, 8.822561741677553471, -79.65000000000004832 ) ) ;
#253047=CARTESIAN_POINT ( 'NONE',  ( -16.97683809663752186, 9.850000000011137402, -87.09763598180373378 ) ) ;
#253405=FACE_OUTER_BOUND ( 'NONE', #167294, .T. ) ;
#253649=ORIENTED_EDGE ( 'NONE', *, *, #8410, .T. ) ;
#253892=ORIENTED_EDGE ( 'NONE', *, *, #211534, .F. ) ;
#253912=DIRECTION ( 'NONE',  ( 1.073024830501117725E-15, 0.000000000000000000, 1.000000000000000000 ) ) ;
#254035=DIRECTION ( 'NONE',  ( -0.000000000000000000, -0.000000000000000000, -1.000000000000000000 ) ) ;
#254217=DIRECTION ( 'NONE',  ( 0.5932847527679299127, -0.8049926720990051576, 6.366092712777055223E-16 ) ) ;
#254223=CARTESIAN_POINT ( 'NONE',  ( 20.99999999999999645, 9.750000000011137757, -87.85000000000003695 ) ) ;
#254238=CARTESIAN_POINT ( 'NONE',  ( 13.54577453029516043, 9.450602096099677496, -85.44389596309672186 ) ) ;
#254478=EDGE_LOOP ( 'NONE', ( #106892, #178194, #25396, #181820 ) ) ;
#254482=EDGE_CURVE ( 'NONE', #172515, #236242, #187160, .T. ) ;
#254803=EDGE_CURVE ( 'NONE', #177843, #97884, #214108, .T. ) ;
#254903=DIRECTION ( 'NONE',  ( -0.000000000000000000, -0.000000000000000000, -1.000000000000000000 ) ) ;
#254972=CARTESIAN_POINT ( 'NONE',  ( -16.89208623190940273, 9.951577948986638944, -87.85527220321831976 ) ) ;
#255129=PLANE ( 'NONE',  #231487 ) ;
#255139=ORIENTED_EDGE ( 'NONE', *, *, #149451, .F. ) ;
#255468=CARTESIAN_POINT ( 'NONE',  ( 18.39999999999999503, 11.47316190337363828, -79.65000000000004832 ) ) ;
#255731=PLANE ( 'NONE',  #201934 ) ;
#255886=STYLED_ITEM ( 'NONE', ( #218746 ), #197609 ) ;
#255974=VECTOR ( 'NONE', #1646, 1000.000000000000000 ) ;
#256100=VECTOR ( 'NONE', #21239, 1000.000000000000000 ) ;
#256186=CARTESIAN_POINT ( 'NONE',  ( -16.77902162784673834, 9.946419257218996890, -79.66199124406939802 ) ) ;
#256211=EDGE_CURVE ( 'NONE', #155242, #219674, #156773, .T. ) ;
#256260=COLOUR_RGB ( '', 0.66274510, 0.83137255, 0.94901961) ;
#256331=ORIENTED_EDGE ( 'NONE', *, *, #201517, .T. ) ;
#256403=CARTESIAN_POINT ( 'NONE',  ( -16.87036670365549895, 9.989418819312803066, -79.52043988269799968 ) ) ;
#256728=CARTESIAN_POINT ( 'NONE',  ( -18.40000000000000213, 5.650000000011139001, -79.65000000000004832 ) ) ;
#256738=CARTESIAN_POINT ( 'NONE',  ( 12.60053434924910043, 9.389534562357859215, -82.67480930438998143 ) ) ;
#257021=EDGE_CURVE ( 'NONE', #108503, #199040, #6195, .T. ) ;
#257033=EDGE_CURVE ( 'NONE', #233341, #146715, #205674, .T. ) ;
#257157=CARTESIAN_POINT ( 'NONE',  ( 23.24999999999999645, 5.650000000011139001, -79.65000000000004832 ) ) ;
#257182=CARTESIAN_POINT ( 'NONE',  ( -16.87683809663752399, 9.850000000011123191, -80.40236401819653622 ) ) ;
#257217=CARTESIAN_POINT ( 'NONE',  ( -16.85312841634287651, 9.913606177331358182, -79.89717313329258275 ) ) ;
#257336=ORIENTED_EDGE ( 'NONE', *, *, #206507, .F. ) ;
#257345=CARTESIAN_POINT ( 'NONE',  ( -23.25000000000000355, 11.75000000001113953, -91.25000000000005684 ) ) ;
#257356=ORIENTED_EDGE ( 'NONE', *, *, #120089, .T. ) ;
#257419=EDGE_CURVE ( 'NONE', #134584, #77128, #184527, .T. ) ;
#257457=EDGE_CURVE ( 'NONE', #146336, #28760, #171232, .T. ) ;
#257580=FACE_OUTER_BOUND ( 'NONE', #82165, .T. ) ;
#257766=PRODUCT ( 'Snap Open Cable Crossbars 3', 'Snap Open Cable Crossbars 3', '', ( #123763 ) ) ;
#257923=PLANE ( 'NONE',  #216209 ) ;
ENDSEC;
END-ISO-10303-21;
